ISO-10303-21;
HEADER;
FILE_DESCRIPTION (('STEP AP214'),
    '1' );
FILE_NAME ('needle roller bearing_nh_iso_ISO 3245 - 3022D - 20,SI,NC,20.step',
    '2026-10-08T11:45:07',
    ( '' ),
    ( '' ),
    'SwSTEP 2.0',
    'SolidWorks 2026',
    '' );
FILE_SCHEMA (( 'AUTOMOTIVE_DESIGN' ));
ENDSEC;

DATA;
#58=CARTESIAN_POINT ( 'NONE',  ( -6.076000000000004952, 19.11697999999999809, 0.000000000000000000 ) ) ;
#144=ORIENTED_EDGE ( 'NONE', *, *, #10315, .T. ) ;
#318=CARTESIAN_POINT ( 'NONE',  ( -6.004904395537136175, 0.000000000000000000, 0.000000000000000000 ) ) ;
#320=CIRCLE ( 'NONE', #19206, 15.08402000000000065 ) ;
#351=CYLINDRICAL_SURFACE ( 'NONE', #6056, 18.77999999999999403 ) ;
#387=ADVANCED_FACE ( 'NONE', ( #37740 ), #10941, .T. ) ;
#467=ORIENTED_EDGE ( 'NONE', *, *, #36751, .F. ) ;
#516=AXIS2_PLACEMENT_3D ( 'NONE', #26547, #20038, #33303 ) ;
#534=LINE ( 'NONE', #37619, #35342 ) ;
#581=DIRECTION ( 'NONE',  ( 0.000000000000000000, 1.000000000000000000, 0.000000000000000000 ) ) ;
#590=DIRECTION ( 'NONE',  ( 1.000000000000000000, 1.836909530733573776E-16, 0.000000000000000000 ) ) ;
#689=CARTESIAN_POINT ( 'NONE',  ( 6.199999999999997513, 18.78000000000008285, 0.000000000000000000 ) ) ;
#724=DIRECTION ( 'NONE',  ( -1.000000000000000000, 0.000000000000000000, 0.000000000000000000 ) ) ;
#918=DIRECTION ( 'NONE',  ( 0.000000000000000000, 0.000000000000000000, 1.000000000000000000 ) ) ;
#1030=CARTESIAN_POINT ( 'NONE',  ( -6.200000000000001066, 18.77999999999999758, 0.000000000000000000 ) ) ;
#1081=DIRECTION ( 'NONE',  ( 1.000000000000000000, 1.836909530733573776E-16, 0.000000000000000000 ) ) ;
#1153=ORIENTED_EDGE ( 'NONE', *, *, #18819, .F. ) ;
#1200=ADVANCED_FACE ( 'NONE', ( #6039 ), #15892, .F. ) ;
#1243=PLANE ( 'NONE',  #19484 ) ;
#1376=CARTESIAN_POINT ( 'NONE',  ( 6.075999999999997847, 0.000000000000000000, 0.000000000000000000 ) ) ;
#1386=CARTESIAN_POINT ( 'NONE',  ( -5.991980000000000750, 0.000000000000000000, 0.000000000000000000 ) ) ;
#1432=CARTESIAN_POINT ( 'NONE',  ( -6.599999999999997868, 20.00000000000000000, 0.000000000000000000 ) ) ;
#1510=VERTEX_POINT ( 'NONE', #38709 ) ;
#1562=AXIS2_PLACEMENT_3D ( 'NONE', #17234, #10209, #40722 ) ;
#1591=EDGE_LOOP ( 'NONE', ( #7231, #22635, #19798, #19757 ) ) ;
#1706=EDGE_CURVE ( 'NONE', #19229, #32995, #9544, .T. ) ;
#1710=DIRECTION ( 'NONE',  ( 0.000000000000000000, 0.000000000000000000, 1.000000000000000000 ) ) ;
#1731=VECTOR ( 'NONE', #38363, 1000.000000000000000 ) ;
#1743=ORIENTED_EDGE ( 'NONE', *, *, #6496, .F. ) ;
#1781=ORIENTED_EDGE ( 'NONE', *, *, #20661, .T. ) ;
#1829=TOROIDAL_SURFACE ( 'NONE', #8128, 19.11697999999999809, 0.08401999999999931745 ) ;
#1879=DIRECTION ( 'NONE',  ( 0.000000000000000000, -1.224646799147338663E-16, 1.000000000000000000 ) ) ;
#1927=DIRECTION ( 'NONE',  ( -1.734723475976807341E-16, 1.000000000000000000, 0.000000000000000000 ) ) ;
#1954=AXIS2_PLACEMENT_3D ( 'NONE', #23607, #40343, #27284 ) ;
#2027=DIRECTION ( 'NONE',  ( 1.000000000000000000, 1.836909530733573776E-16, 0.000000000000000000 ) ) ;
#2032=CIRCLE ( 'NONE', #32689, 0.08401999999999888724 ) ;
#2085=DIRECTION ( 'NONE',  ( -1.000000000000000000, -1.836909530733573776E-16, 0.000000000000000000 ) ) ;
#2159=TOROIDAL_SURFACE ( 'NONE', #17537, 15.08402000000000065, 0.08401999999999888724 ) ;
#2207=AXIS2_PLACEMENT_3D ( 'NONE', #20856, #34105, #23680 ) ;
#2217=VERTEX_POINT ( 'NONE', #31181 ) ;
#2292=DIRECTION ( 'NONE',  ( 1.000000000000000000, 1.836909530733573776E-16, 0.000000000000000000 ) ) ;
#2368=AXIS2_PLACEMENT_3D ( 'NONE', #22260, #29856, #16319 ) ;
#2484=ORIENTED_EDGE ( 'NONE', *, *, #36161, .F. ) ;
#2487=CARTESIAN_POINT ( 'NONE',  ( -6.600000000000001421, 3.469446951953649688E-15, 0.000000000000000000 ) ) ;
#2495=AXIS2_PLACEMENT_3D ( 'NONE', #29498, #2634, #9203 ) ;
#2504=DIRECTION ( 'NONE',  ( 1.836909530733573776E-16, -1.000000000000000000, 0.000000000000000000 ) ) ;
#2576=CARTESIAN_POINT ( 'NONE',  ( -6.999999999999995559, -18.77999999999999048, 2.299886688798728717E-15 ) ) ;
#2616=ORIENTED_EDGE ( 'NONE', *, *, #32720, .T. ) ;
#2634=DIRECTION ( 'NONE',  ( -1.000000000000000000, 0.000000000000000000, 0.000000000000000000 ) ) ;
#2654=FACE_OUTER_BOUND ( 'NONE', #11047, .T. ) ;
#2680=ORIENTED_EDGE ( 'NONE', *, *, #12143, .T. ) ;
#2689=EDGE_LOOP ( 'NONE', ( #27212, #33679, #22248, #7737, #33947 ) ) ;
#2759=VERTEX_POINT ( 'NONE', #42193 ) ;
#2830=CARTESIAN_POINT ( 'NONE',  ( -6.004904395537136175, 0.000000000000000000, 0.000000000000000000 ) ) ;
#2839=ADVANCED_FACE ( 'NONE', ( #38717 ), #11930, .F. ) ;
#2994=ORIENTED_EDGE ( 'NONE', *, *, #10680, .F. ) ;
#3151=DIRECTION ( 'NONE',  ( -3.469446951953614682E-16, 1.000000000000000000, 0.000000000000000000 ) ) ;
#3163=TOROIDAL_SURFACE ( 'NONE', #8769, 19.59999999999999076, 0.4000000000000001887 ) ;
#3177=AXIS2_PLACEMENT_3D ( 'NONE', #25955, #9574, #39214 ) ;
#3209=EDGE_CURVE ( 'NONE', #21160, #38331, #18501, .T. ) ;
#3218=AXIS2_PLACEMENT_3D ( 'NONE', #42628, #39144, #9485 ) ;
#3254=DIRECTION ( 'NONE',  ( 1.000000000000000000, 1.836909530733573776E-16, 0.000000000000000000 ) ) ;
#3272=CARTESIAN_POINT ( 'NONE',  ( 5.991980000000000750, 0.000000000000000000, 0.000000000000000000 ) ) ;
#3305=EDGE_LOOP ( 'NONE', ( #11083, #15228, #7574, #14144 ) ) ;
#3376=EDGE_CURVE ( 'NONE', #40002, #17054, #320, .T. ) ;
#3477=CARTESIAN_POINT ( 'NONE',  ( -6.600000000000004974, 19.59999999999999787, 0.000000000000000000 ) ) ;
#3478=EDGE_LOOP ( 'NONE', ( #7369, #39543, #10566, #17396 ) ) ;
#3678=ADVANCED_FACE ( 'NONE', ( #30370 ), #10766, .T. ) ;
#3715=DIRECTION ( 'NONE',  ( -1.000000000000000000, 0.000000000000000000, 0.000000000000000000 ) ) ;
#3730=DIRECTION ( 'NONE',  ( -1.000000000000000000, -1.836909530733573776E-16, 0.000000000000000000 ) ) ;
#3745=ORIENTED_EDGE ( 'NONE', *, *, #21121, .T. ) ;
#3763=FACE_BOUND ( 'NONE', #19743, .T. ) ;
#3807=DIRECTION ( 'NONE',  ( 1.000000000000000000, 0.000000000000000000, 0.000000000000000000 ) ) ;
#3836=CARTESIAN_POINT ( 'NONE',  ( -31.75000000000000000, 0.000000000000000000, 0.000000000000000000 ) ) ;
#3852=CARTESIAN_POINT ( 'NONE',  ( 0.000000000000000000, 0.000000000000000000, 0.000000000000000000 ) ) ;
#3855=EDGE_LOOP ( 'NONE', ( #1743, #18204, #28214, #22067, #41871 ) ) ;
#3947=CARTESIAN_POINT ( 'NONE',  ( 6.004904395537136175, 0.000000000000000000, 0.000000000000000000 ) ) ;
#3993=FACE_BOUND ( 'NONE', #10577, .T. ) ;
#4005=ORIENTED_EDGE ( 'NONE', *, *, #30689, .F. ) ;
#4034=VERTEX_POINT ( 'NONE', #29047 ) ;
#4088=DIRECTION ( 'NONE',  ( -1.836909530733573776E-16, 1.000000000000000000, 0.000000000000000000 ) ) ;
#4123=FACE_OUTER_BOUND ( 'NONE', #31546, .T. ) ;
#4226=ORIENTED_EDGE ( 'NONE', *, *, #28900, .F. ) ;
#4272=CARTESIAN_POINT ( 'NONE',  ( 6.075999999999998735, 0.000000000000000000, 15.08402000000000065 ) ) ;
#4294=VERTEX_POINT ( 'NONE', #41926 ) ;
#4416=( GEOMETRIC_REPRESENTATION_CONTEXT ( 3 ) GLOBAL_UNCERTAINTY_ASSIGNED_CONTEXT ( ( #39027 ) ) GLOBAL_UNIT_ASSIGNED_CONTEXT ( ( #41067, #7495, #34112 ) ) REPRESENTATION_CONTEXT ( 'NONE', 'WORKASPACE' ) );
#4601=DIRECTION ( 'NONE',  ( 1.000000000000000000, 1.836909530733573776E-16, 0.000000000000000000 ) ) ;
#4660=ORIENTED_EDGE ( 'NONE', *, *, #38394, .F. ) ;
#4664=DIRECTION ( 'NONE',  ( 0.000000000000000000, 0.000000000000000000, 1.000000000000000000 ) ) ;
#4911=EDGE_CURVE ( 'NONE', #39320, #41075, #14706, .T. ) ;
#4934=AXIS2_PLACEMENT_3D ( 'NONE', #16468, #43043, #7252 ) ;
#5043=DIRECTION ( 'NONE',  ( 1.000000000000000000, 1.836909530733573776E-16, 0.000000000000000000 ) ) ;
#5058=ORIENTED_EDGE ( 'NONE', *, *, #3376, .F. ) ;
#5074=FACE_OUTER_BOUND ( 'NONE', #3855, .T. ) ;
#5082=DIRECTION ( 'NONE',  ( -1.000000000000000000, 0.000000000000000000, 0.000000000000000000 ) ) ;
#5195=AXIS2_PLACEMENT_3D ( 'NONE', #34023, #16675, #19945 ) ;
#5205=CARTESIAN_POINT ( 'NONE',  ( -6.004904395537136175, 0.000000000000000000, 0.000000000000000000 ) ) ;
#5302=SURFACE_SIDE_STYLE ('',( #28464 ) ) ;
#5342=VERTEX_POINT ( 'NONE', #19758 ) ;
#5349=AXIS2_PLACEMENT_3D ( 'NONE', #28953, #2085, #2504 ) ;
#5359=DIRECTION ( 'NONE',  ( 0.000000000000000000, 0.000000000000000000, 1.000000000000000000 ) ) ;
#5429=DIRECTION ( 'NONE',  ( 1.000000000000000000, 1.836909530733573776E-16, 0.000000000000000000 ) ) ;
#5488=CARTESIAN_POINT ( 'NONE',  ( -6.999999999999999112, 4.546351088565595293E-15, 0.000000000000000000 ) ) ;
#5494=EDGE_CURVE ( 'NONE', #40931, #12750, #21545, .T. ) ;
#5519=VERTEX_POINT ( 'NONE', #18438 ) ;
#5589=EDGE_LOOP ( 'NONE', ( #21616, #10933, #41941, #25454 ) ) ;
#5597=DIRECTION ( 'NONE',  ( 1.000000000000000000, 1.836909530733573776E-16, 0.000000000000000000 ) ) ;
#5762=EDGE_CURVE ( 'NONE', #39595, #15674, #11706, .T. ) ;
#5798=DIRECTION ( 'NONE',  ( -2.249565377136137858E-32, 1.224646799147353207E-16, 1.000000000000000000 ) ) ;
#5801=CARTESIAN_POINT ( 'NONE',  ( 6.999999999999999112, 7.118024431592597790E-15, 0.000000000000000000 ) ) ;
#5994=CIRCLE ( 'NONE', #23440, 0.08401999999999715252 ) ;
#6038=AXIS2_PLACEMENT_3D ( 'NONE', #13018, #39798, #20010 ) ;
#6039=FACE_OUTER_BOUND ( 'NONE', #3478, .T. ) ;
#6040=DIRECTION ( 'NONE',  ( -1.770125995894701942E-16, 1.000000000000000000, 0.000000000000000000 ) ) ;
#6056=AXIS2_PLACEMENT_3D ( 'NONE', #3836, #13285, #581 ) ;
#6071=DIRECTION ( 'NONE',  ( -1.836909530733573776E-16, 1.000000000000000000, 0.000000000000000000 ) ) ;
#6213=FACE_OUTER_BOUND ( 'NONE', #24577, .T. ) ;
#6228=FACE_OUTER_BOUND ( 'NONE', #29374, .T. ) ;
#6482=ORIENTED_EDGE ( 'NONE', *, *, #21725, .T. ) ;
#6491=DIRECTION ( 'NONE',  ( -1.734723475976807834E-16, 1.000000000000000000, 0.000000000000000000 ) ) ;
#6496=EDGE_CURVE ( 'NONE', #38321, #32995, #8827, .T. ) ;
#6497=ORIENTED_EDGE ( 'NONE', *, *, #13001, .T. ) ;
#6509=DIRECTION ( 'NONE',  ( -1.847415842360817977E-16, 1.000000000000000000, 0.000000000000000000 ) ) ;
#6537=ORIENTED_EDGE ( 'NONE', *, *, #21725, .F. ) ;
#6592=CARTESIAN_POINT ( 'NONE',  ( 6.200000000000001066, 19.19999999999999929, 0.000000000000000000 ) ) ;
#6619=ADVANCED_FACE ( 'NONE', ( #3993, #30428 ), #14077, .F. ) ;
#6760=PRODUCT_DEFINITION_SHAPE ( 'NONE', 'NONE',  #8157 ) ;
#6852=DIRECTION ( 'NONE',  ( -1.000000000000000000, 0.000000000000000000, 0.000000000000000000 ) ) ;
#6876=DIRECTION ( 'NONE',  ( 1.000000000000000000, 1.836909530733573776E-16, 0.000000000000000000 ) ) ;
#7028=CARTESIAN_POINT ( 'NONE',  ( -5.991980000000000750, 2.341154836636396601E-15, -19.11697999999999809 ) ) ;
#7029=ADVANCED_FACE ( 'NONE', ( #16005 ), #2159, .T. ) ;
#7126=ORIENTED_EDGE ( 'NONE', *, *, #27280, .F. ) ;
#7180=AXIS2_PLACEMENT_3D ( 'NONE', #41986, #15423, #15622 ) ;
#7231=ORIENTED_EDGE ( 'NONE', *, *, #30431, .F. ) ;
#7252=DIRECTION ( 'NONE',  ( 0.000000000000000000, 0.000000000000000000, 1.000000000000000000 ) ) ;
#7316=ORIENTED_EDGE ( 'NONE', *, *, #6496, .T. ) ;
#7369=ORIENTED_EDGE ( 'NONE', *, *, #29885, .F. ) ;
#7495=( NAMED_UNIT ( * ) PLANE_ANGLE_UNIT ( ) SI_UNIT ( $, .RADIAN. ) );
#7574=ORIENTED_EDGE ( 'NONE', *, *, #36768, .F. ) ;
#7737=ORIENTED_EDGE ( 'NONE', *, *, #10680, .T. ) ;
#7792=FACE_BOUND ( 'NONE', #25624, .T. ) ;
#7806=AXIS2_PLACEMENT_3D ( 'NONE', #32551, #9843, #36440 ) ;
#7878=SHAPE_REPRESENTATION ( 'needle roller bearing_nh_iso_ISO 3245 - 3022D - 20,SI,NC,20', ( #13552 ), #4416 ) ;
#7886=DIRECTION ( 'NONE',  ( 0.000000000000000000, 0.000000000000000000, 1.000000000000000000 ) ) ;
#7896=ADVANCED_FACE ( 'NONE', ( #22483, #25752 ), #9335, .T. ) ;
#7934=CARTESIAN_POINT ( 'NONE',  ( 6.075999999999997847, 0.000000000000000000, 0.000000000000000000 ) ) ;
#7974=ORIENTED_EDGE ( 'NONE', *, *, #14856, .F. ) ;
#8049=DIRECTION ( 'NONE',  ( -1.000000000000000000, 0.000000000000000000, 0.000000000000000000 ) ) ;
#8128=AXIS2_PLACEMENT_3D ( 'NONE', #31021, #3715, #20166 ) ;
#8129=CARTESIAN_POINT ( 'NONE',  ( -6.075999999999997847, 0.000000000000000000, 0.000000000000000000 ) ) ;
#8157=PRODUCT_DEFINITION ( 'UNKNOWN', '', #36488, #32497 ) ;
#8185=EDGE_LOOP ( 'NONE', ( #21416, #7316, #16335, #467, #4660 ) ) ;
#8237=DIRECTION ( 'NONE',  ( -2.249565377136137858E-32, 1.224646799147353207E-16, 1.000000000000000000 ) ) ;
#8260=CYLINDRICAL_SURFACE ( 'NONE', #36394, 19.19999999999999574 ) ;
#8391=CARTESIAN_POINT ( 'NONE',  ( 6.004904395537136175, 0.000000000000000000, 0.000000000000000000 ) ) ;
#8409=ORIENTED_EDGE ( 'NONE', *, *, #25232, .F. ) ;
#8416=AXIS2_PLACEMENT_3D ( 'NONE', #318, #3807, #30253 ) ;
#8457=CARTESIAN_POINT ( 'NONE',  ( 6.075999999999997847, 2.346238345499656945E-15, -19.11697999999999809 ) ) ;
#8554=ORIENTED_EDGE ( 'NONE', *, *, #14856, .T. ) ;
#8669=ORIENTED_EDGE ( 'NONE', *, *, #30083, .F. ) ;
#8769=AXIS2_PLACEMENT_3D ( 'NONE', #40735, #20953, #4088 ) ;
#8827=CIRCLE ( 'NONE', #3218, 0.08402000000000062196 ) ;
#8960=CIRCLE ( 'NONE', #9672, 19.19999999999999574 ) ;
#8969=CARTESIAN_POINT ( 'NONE',  ( -6.999999999999999112, 4.546351088565595293E-15, 0.000000000000000000 ) ) ;
#8987=CIRCLE ( 'NONE', #33369, 15.08402000000000065 ) ;
#8989=AXIS2_PLACEMENT_3D ( 'NONE', #15256, #28329, #22435 ) ;
#9073=FACE_BOUND ( 'NONE', #43129, .T. ) ;
#9080=CARTESIAN_POINT ( 'NONE',  ( -6.599999999999994316, 4.619827469794975478E-15, 0.000000000000000000 ) ) ;
#9100=ORIENTED_EDGE ( 'NONE', *, *, #18220, .T. ) ;
#9123=FACE_OUTER_BOUND ( 'NONE', #33513, .T. ) ;
#9203=DIRECTION ( 'NONE',  ( 0.000000000000000000, 0.000000000000000000, 1.000000000000000000 ) ) ;
#9233=ORIENTED_EDGE ( 'NONE', *, *, #3209, .T. ) ;
#9256=AXIS2_PLACEMENT_3D ( 'NONE', #32854, #38963, #3151 ) ;
#9295=VECTOR ( 'NONE', #40781, 1000.000000000000000 ) ;
#9328=FILL_AREA_STYLE ('',( #36365 ) ) ;
#9335=PLANE ( 'NONE',  #18231 ) ;
#9342=EDGE_CURVE ( 'NONE', #11045, #16762, #14839, .T. ) ;
#9440=VERTEX_POINT ( 'NONE', #33551 ) ;
#9453=VERTEX_POINT ( 'NONE', #36595 ) ;
#9475=EDGE_CURVE ( 'NONE', #16762, #1510, #20418, .T. ) ;
#9485=DIRECTION ( 'NONE',  ( 0.000000000000000000, -1.224646799147313518E-16, 1.000000000000000000 ) ) ;
#9497=( GEOMETRIC_REPRESENTATION_CONTEXT ( 3 ) GLOBAL_UNCERTAINTY_ASSIGNED_CONTEXT ( ( #13462 ) ) GLOBAL_UNIT_ASSIGNED_CONTEXT ( ( #13282, #35934, #19620 ) ) REPRESENTATION_CONTEXT ( 'NONE', 'WORKASPACE' ) );
#9544=CIRCLE ( 'NONE', #33922, 19.19999999999999574 ) ;
#9574=DIRECTION ( 'NONE',  ( -1.000000000000000000, 0.000000000000000000, 0.000000000000000000 ) ) ;
#9594=CARTESIAN_POINT ( 'NONE',  ( 6.999999999999999112, 7.118024431592597790E-15, 0.000000000000000000 ) ) ;
#9623=CIRCLE ( 'NONE', #1954, 0.08402000000000062196 ) ;
#9645=CIRCLE ( 'NONE', #22217, 19.19999999999999574 ) ;
#9672=AXIS2_PLACEMENT_3D ( 'NONE', #29700, #3254, #36870 ) ;
#9703=CARTESIAN_POINT ( 'NONE',  ( 5.991980000000000750, 0.000000000000000000, 0.000000000000000000 ) ) ;
#9768=ADVANCED_FACE ( 'NONE', ( #22875 ), #33062, .T. ) ;
#9843=DIRECTION ( 'NONE',  ( 1.000000000000000000, 1.836909530733573776E-16, 0.000000000000000000 ) ) ;
#9860=DIRECTION ( 'NONE',  ( 1.000000000000000000, 1.836909530733573776E-16, 0.000000000000000000 ) ) ;
#9892=PRODUCT ( 'needle roller bearing_nh_iso_ISO 3245 - 3022D - 20,SI,NC,20', 'needle roller bearing_nh_iso_ISO 3245 - 3022D - 20,SI,NC,20', '', ( #34706 ) ) ;
#10069=ORIENTED_EDGE ( 'NONE', *, *, #28986, .T. ) ;
#10142=ORIENTED_EDGE ( 'NONE', *, *, #5762, .F. ) ;
#10162=CARTESIAN_POINT ( 'NONE',  ( 7.000000000000006217, 7.118024431592600946E-15, 0.000000000000000000 ) ) ;
#10168=AXIS2_PLACEMENT_3D ( 'NONE', #7934, #724, #24122 ) ;
#10191=DIRECTION ( 'NONE',  ( 1.000000000000000000, 1.836909530733573776E-16, 0.000000000000000000 ) ) ;
#10209=DIRECTION ( 'NONE',  ( 0.000000000000000000, 0.000000000000000000, -1.000000000000000000 ) ) ;
#10213=DIRECTION ( 'NONE',  ( 1.000000000000000000, 0.000000000000000000, 0.000000000000000000 ) ) ;
#10239=CIRCLE ( 'NONE', #40279, 0.4000000000000010214 ) ;
#10256=CYLINDRICAL_SURFACE ( 'NONE', #30543, 19.19999999999999574 ) ;
#10267=AXIS2_PLACEMENT_3D ( 'NONE', #3477, #19476, #22538 ) ;
#10315=EDGE_CURVE ( 'NONE', #9453, #17146, #16807, .T. ) ;
#10357=ORIENTED_EDGE ( 'NONE', *, *, #41900, .F. ) ;
#10391=CIRCLE ( 'NONE', #8989, 18.77999999999999048 ) ;
#10566=ORIENTED_EDGE ( 'NONE', *, *, #27280, .T. ) ;
#10569=PLANE ( 'NONE',  #28952 ) ;
#10577=EDGE_LOOP ( 'NONE', ( #25844, #16959 ) ) ;
#10583=CARTESIAN_POINT ( 'NONE',  ( -25.39999999999999147, 0.000000000000000000, 15.00000000000000000 ) ) ;
#10654=FACE_OUTER_BOUND ( 'NONE', #27435, .T. ) ;
#10680=EDGE_CURVE ( 'NONE', #5519, #37013, #42562, .T. ) ;
#10725=CARTESIAN_POINT ( 'NONE',  ( 6.004904395537136175, -19.19999999999999574, 2.351321854362918473E-15 ) ) ;
#10766=TOROIDAL_SURFACE ( 'NONE', #16348, 15.08402000000000065, 0.08402000000000148239 ) ;
#10774=CARTESIAN_POINT ( 'NONE',  ( -6.199999999999997513, 4.693303851024319376E-15, 0.000000000000000000 ) ) ;
#10781=DIRECTION ( 'NONE',  ( -1.000000000000000000, 0.000000000000000000, 0.000000000000000000 ) ) ;
#10784=ORIENTED_EDGE ( 'NONE', *, *, #15966, .T. ) ;
#10866=DIRECTION ( 'NONE',  ( -1.000000000000000000, 0.000000000000000000, 0.000000000000000000 ) ) ;
#10920=ADVANCED_BREP_SHAPE_REPRESENTATION ( '', ( #28662, #13552 ), #4416 ) ;
#10933=ORIENTED_EDGE ( 'NONE', *, *, #32405, .F. ) ;
#10941=CYLINDRICAL_SURFACE ( 'NONE', #14336, 19.99999999999999645 ) ;
#10943=DIRECTION ( 'NONE',  ( 1.000000000000000000, 1.836909530733573776E-16, 0.000000000000000000 ) ) ;
#11045=VERTEX_POINT ( 'NONE', #33070 ) ;
#11047=EDGE_LOOP ( 'NONE', ( #10357, #13995, #8554, #41732 ) ) ;
#11083=ORIENTED_EDGE ( 'NONE', *, *, #32405, .T. ) ;
#11098=CIRCLE ( 'NONE', #22955, 18.77999999999999048 ) ;
#11473=CLOSED_SHELL ( 'NONE', ( #38210, #14138, #42970, #2839, #3678, #12689, #40438, #387, #41407, #1200, #13973, #30064, #32588, #25581, #27848, #34654, #35018, #27652, #9768, #33082, #7896, #17774, #15634, #17603, #16218, #7029, #20470, #41346, #18710, #6619 ) ) ;
#11518=CARTESIAN_POINT ( 'NONE',  ( -6.599999999999997868, -19.59999999999999076, 2.400307726328811901E-15 ) ) ;
#11542=FACE_OUTER_BOUND ( 'NONE', #2689, .T. ) ;
#11556=EDGE_CURVE ( 'NONE', #32995, #21160, #25943, .T. ) ;
#11706=CIRCLE ( 'NONE', #13785, 14.99999999999999822 ) ;
#11775=AXIS2_PLACEMENT_3D ( 'NONE', #689, #3730, #31265 ) ;
#11886=CARTESIAN_POINT ( 'NONE',  ( -6.075999999999997847, 0.000000000000000000, 0.000000000000000000 ) ) ;
#11930=CYLINDRICAL_SURFACE ( 'NONE', #16466, 15.00000000000000000 ) ;
#11950=CARTESIAN_POINT ( 'NONE',  ( -6.999999999999995559, -19.59999999999999076, 2.424800662311759010E-15 ) ) ;
#11969=ORIENTED_EDGE ( 'NONE', *, *, #5494, .F. ) ;
#11984=ORIENTED_EDGE ( 'NONE', *, *, #30603, .F. ) ;
#12097=DIRECTION ( 'NONE',  ( 1.000000000000000000, 1.836909530733573776E-16, 0.000000000000000000 ) ) ;
#12122=( GEOMETRIC_REPRESENTATION_CONTEXT ( 3 ) GLOBAL_UNCERTAINTY_ASSIGNED_CONTEXT ( ( #18604 ) ) GLOBAL_UNIT_ASSIGNED_CONTEXT ( ( #12510, #14936, #38883 ) ) REPRESENTATION_CONTEXT ( 'NONE', 'WORKASPACE' ) );
#12143=EDGE_CURVE ( 'NONE', #20227, #40931, #42635, .T. ) ;
#12297=FILL_AREA_STYLE ('',( #42138 ) ) ;
#12419=CARTESIAN_POINT ( 'NONE',  ( -31.75000000000000711, 19.99999999999999645, 0.000000000000000000 ) ) ;
#12457=EDGE_LOOP ( 'NONE', ( #17125, #27128 ) ) ;
#12510=( LENGTH_UNIT ( ) NAMED_UNIT ( * ) SI_UNIT ( .MILLI., .METRE. ) );
#12606=ORIENTED_EDGE ( 'NONE', *, *, #33327, .F. ) ;
#12624=ORIENTED_EDGE ( 'NONE', *, *, #20500, .F. ) ;
#12658=CARTESIAN_POINT ( 'NONE',  ( 6.600000000000008527, 6.938893903907228378E-15, 0.000000000000000000 ) ) ;
#12670=CIRCLE ( 'NONE', #18283, 19.11697999999999809 ) ;
#12688=ORIENTED_EDGE ( 'NONE', *, *, #4911, .F. ) ;
#12689=ADVANCED_FACE ( 'NONE', ( #43019 ), #27489, .F. ) ;
#12699=AXIS2_PLACEMENT_3D ( 'NONE', #3947, #41035, #7886 ) ;
#12750=VERTEX_POINT ( 'NONE', #37282 ) ;
#12802=ORIENTED_EDGE ( 'NONE', *, *, #17041, .F. ) ;
#12838=PRESENTATION_STYLE_ASSIGNMENT (( #33102 ) ) ;
#12972=EDGE_LOOP ( 'NONE', ( #23326, #32143, #10142, #8669 ) ) ;
#13001=EDGE_CURVE ( 'NONE', #9453, #15674, #34883, .T. ) ;
#13003=AXIS2_PLACEMENT_3D ( 'NONE', #10162, #25922, #6040 ) ;
#13018=CARTESIAN_POINT ( 'NONE',  ( 6.199999999999997513, 6.971071669133949438E-15, 0.000000000000000000 ) ) ;
#13104=DIRECTION ( 'NONE',  ( 1.000000000000000000, 1.836909530733573776E-16, 0.000000000000000000 ) ) ;
#13125=CIRCLE ( 'NONE', #31247, 18.77999999999999403 ) ;
#13130=DIRECTION ( 'NONE',  ( 1.000000000000000000, 1.836909530733573776E-16, 0.000000000000000000 ) ) ;
#13180=ORIENTED_EDGE ( 'NONE', *, *, #36768, .T. ) ;
#13198=EDGE_LOOP ( 'NONE', ( #23027, #8409 ) ) ;
#13243=CIRCLE ( 'NONE', #27191, 19.11697999999999809 ) ;
#13282=( LENGTH_UNIT ( ) NAMED_UNIT ( * ) SI_UNIT ( .MILLI., .METRE. ) );
#13285=DIRECTION ( 'NONE',  ( 1.000000000000000000, 1.836909530733573776E-16, 0.000000000000000000 ) ) ;
#13345=EDGE_CURVE ( 'NONE', #9453, #40002, #23411, .T. ) ;
#13392=ORIENTED_EDGE ( 'NONE', *, *, #20621, .F. ) ;
#13405=VERTEX_POINT ( 'NONE', #34834 ) ;
#13462=UNCERTAINTY_MEASURE_WITH_UNIT (LENGTH_MEASURE( 1.000000000000000082E-05 ), #13282, 'distance_accuracy_value', 'NONE');
#13552=AXIS2_PLACEMENT_3D ( 'NONE', #3852, #14597, #10213 ) ;
#13564=VECTOR ( 'NONE', #35466, 1000.000000000000000 ) ;
#13611=DIRECTION ( 'NONE',  ( 0.000000000000000000, -1.224646799147364054E-16, 1.000000000000000000 ) ) ;
#13631=CARTESIAN_POINT ( 'NONE',  ( 6.004904395537136175, 0.000000000000000000, 0.000000000000000000 ) ) ;
#13740=EDGE_CURVE ( 'NONE', #2759, #38321, #33843, .T. ) ;
#13785=AXIS2_PLACEMENT_3D ( 'NONE', #23634, #20151, #36666 ) ;
#13812=DIRECTION ( 'NONE',  ( -1.000000000000000000, 0.000000000000000000, 0.000000000000000000 ) ) ;
#13973=ADVANCED_FACE ( 'NONE', ( #19721 ), #16673, .F. ) ;
#13986=CARTESIAN_POINT ( 'NONE',  ( -31.75000000000000000, 0.000000000000000000, 0.000000000000000000 ) ) ;
#13995=ORIENTED_EDGE ( 'NONE', *, *, #28986, .F. ) ;
#14026=DIRECTION ( 'NONE',  ( -1.807003620809174385E-16, 1.000000000000000000, 0.000000000000000000 ) ) ;
#14077=PLANE ( 'NONE',  #37377 ) ;
#14138=ADVANCED_FACE ( 'NONE', ( #14237 ), #1829, .T. ) ;
#14144=ORIENTED_EDGE ( 'NONE', *, *, #19464, .F. ) ;
#14192=ORIENTED_EDGE ( 'NONE', *, *, #28082, .T. ) ;
#14237=FACE_OUTER_BOUND ( 'NONE', #8185, .T. ) ;
#14288=FACE_OUTER_BOUND ( 'NONE', #18744, .T. ) ;
#14295=ORIENTED_EDGE ( 'NONE', *, *, #30431, .T. ) ;
#14336=AXIS2_PLACEMENT_3D ( 'NONE', #23830, #1081, #34049 ) ;
#14378=AXIS2_PLACEMENT_3D ( 'NONE', #28373, #5429, #1927 ) ;
#14432=ORIENTED_EDGE ( 'NONE', *, *, #25232, .T. ) ;
#14453=ORIENTED_EDGE ( 'NONE', *, *, #24802, .F. ) ;
#14459=ORIENTED_EDGE ( 'NONE', *, *, #20500, .T. ) ;
#14545=AXIS2_PLACEMENT_3D ( 'NONE', #5488, #39480, #35573 ) ;
#14582=EDGE_CURVE ( 'NONE', #29681, #39320, #27664, .T. ) ;
#14597=DIRECTION ( 'NONE',  ( 0.000000000000000000, 0.000000000000000000, 1.000000000000000000 ) ) ;
#14648=EDGE_LOOP ( 'NONE', ( #27209, #14295, #12606, #42492 ) ) ;
#14706=CIRCLE ( 'NONE', #8416, 19.19999999999999574 ) ;
#14725=DIRECTION ( 'NONE',  ( 0.000000000000000000, 0.000000000000000000, 1.000000000000000000 ) ) ;
#14786=CARTESIAN_POINT ( 'NONE',  ( 5.991980000000000750, 0.000000000000000000, 15.00000000000000178 ) ) ;
#14816=TOROIDAL_SURFACE ( 'NONE', #7806, 19.59999999999999432, 0.4000000000000001887 ) ;
#14818=DIRECTION ( 'NONE',  ( -1.000000000000000000, 0.000000000000000000, 0.000000000000000000 ) ) ;
#14826=CARTESIAN_POINT ( 'NONE',  ( -31.75000000000000000, 0.000000000000000000, 0.000000000000000000 ) ) ;
#14839=CIRCLE ( 'NONE', #24625, 19.99999999999999289 ) ;
#14856=EDGE_CURVE ( 'NONE', #24696, #42589, #33481, .T. ) ;
#14936=( NAMED_UNIT ( * ) PLANE_ANGLE_UNIT ( ) SI_UNIT ( $, .RADIAN. ) );
#14993=DIRECTION ( 'NONE',  ( -1.000000000000000000, 0.000000000000000000, 0.000000000000000000 ) ) ;
#15012=CARTESIAN_POINT ( 'NONE',  ( -31.75000000000000711, 19.19999999999999574, 0.000000000000000000 ) ) ;
#15014=DIRECTION ( 'NONE',  ( 0.000000000000000000, 1.000000000000000000, 1.224646799147353207E-16 ) ) ;
#15070=CIRCLE ( 'NONE', #28976, 15.00000000000000178 ) ;
#15228=ORIENTED_EDGE ( 'NONE', *, *, #13345, .T. ) ;
#15256=CARTESIAN_POINT ( 'NONE',  ( 6.199999999999997513, 6.971071669133949438E-15, 0.000000000000000000 ) ) ;
#15275=TOROIDAL_SURFACE ( 'NONE', #21543, 19.11697999999999809, 0.08401999999999801294 ) ;
#15317=DIRECTION ( 'NONE',  ( 0.000000000000000000, -1.000000000000000000, 0.000000000000000000 ) ) ;
#15336=DIRECTION ( 'NONE',  ( -1.807003620809174878E-16, 1.000000000000000000, 0.000000000000000000 ) ) ;
#15369=SURFACE_STYLE_USAGE ( .BOTH. , #5302 ) ;
#15423=DIRECTION ( 'NONE',  ( 1.000000000000000000, 0.000000000000000000, 0.000000000000000000 ) ) ;
#15492=AXIS2_PLACEMENT_3D ( 'NONE', #12658, #22944, #15518 ) ;
#15518=DIRECTION ( 'NONE',  ( -1.836909530733573776E-16, 1.000000000000000000, 0.000000000000000000 ) ) ;
#15520=CIRCLE ( 'NONE', #24590, 18.77999999999999048 ) ;
#15528=SHAPE_DEFINITION_REPRESENTATION ( #6760, #7878 ) ;
#15546=ORIENTED_EDGE ( 'NONE', *, *, #28532, .T. ) ;
#15622=DIRECTION ( 'NONE',  ( 0.000000000000000000, 0.000000000000000000, -1.000000000000000000 ) ) ;
#15634=ADVANCED_FACE ( 'NONE', ( #36266, #19738 ), #33000, .T. ) ;
#15653=DIRECTION ( 'NONE',  ( -1.734723475976807341E-16, 1.000000000000000000, 0.000000000000000000 ) ) ;
#15665=ORIENTED_EDGE ( 'NONE', *, *, #41231, .F. ) ;
#15674=VERTEX_POINT ( 'NONE', #17112 ) ;
#15726=DIRECTION ( 'NONE',  ( 0.000000000000000000, 0.000000000000000000, -1.000000000000000000 ) ) ;
#15761=ORIENTED_EDGE ( 'NONE', *, *, #29885, .T. ) ;
#15785=ORIENTED_EDGE ( 'NONE', *, *, #41231, .T. ) ;
#15797=CARTESIAN_POINT ( 'NONE',  ( -31.75000000000000000, 0.000000000000000000, 0.000000000000000000 ) ) ;
#15810=VECTOR ( 'NONE', #38314, 1000.000000000000000 ) ;
#15892=CYLINDRICAL_SURFACE ( 'NONE', #516, 18.77999999999999403 ) ;
#15950=EDGE_LOOP ( 'NONE', ( #18477, #6497, #42784, #28753 ) ) ;
#15966=EDGE_CURVE ( 'NONE', #30619, #16491, #24334, .T. ) ;
#16005=FACE_OUTER_BOUND ( 'NONE', #37396, .T. ) ;
#16068=CARTESIAN_POINT ( 'NONE',  ( -31.75000000000000000, 18.77999999999999403, 0.000000000000000000 ) ) ;
#16083=DIRECTION ( 'NONE',  ( 0.000000000000000000, -1.000000000000000000, 1.224646799147353207E-16 ) ) ;
#16194=DIRECTION ( 'NONE',  ( 0.000000000000000000, 0.000000000000000000, -1.000000000000000000 ) ) ;
#16218=ADVANCED_FACE ( 'NONE', ( #40348 ), #40778, .F. ) ;
#16304=CARTESIAN_POINT ( 'NONE',  ( 5.991979999999993645, 0.000000000000000000, 19.11697999999999809 ) ) ;
#16319=DIRECTION ( 'NONE',  ( -1.847415842360817484E-16, 1.000000000000000000, 0.000000000000000000 ) ) ;
#16335=ORIENTED_EDGE ( 'NONE', *, *, #1706, .F. ) ;
#16348=AXIS2_PLACEMENT_3D ( 'NONE', #17085, #13812, #30802 ) ;
#16455=EDGE_LOOP ( 'NONE', ( #35786, #23136 ) ) ;
#16466=AXIS2_PLACEMENT_3D ( 'NONE', #38501, #14993, #5359 ) ;
#16468=CARTESIAN_POINT ( 'NONE',  ( 5.991980000000000750, 0.000000000000000000, 0.000000000000000000 ) ) ;
#16473=CIRCLE ( 'NONE', #3177, 15.08402000000000065 ) ;
#16483=ORIENTED_EDGE ( 'NONE', *, *, #30083, .T. ) ;
#16491=VERTEX_POINT ( 'NONE', #1432 ) ;
#16563=AXIS2_PLACEMENT_3D ( 'NONE', #31666, #5043, #15336 ) ;
#16603=ORIENTED_EDGE ( 'NONE', *, *, #28532, .F. ) ;
#16673=CYLINDRICAL_SURFACE ( 'NONE', #24165, 19.19999999999999574 ) ;
#16675=DIRECTION ( 'NONE',  ( 1.000000000000000000, 1.836909530733573776E-16, 0.000000000000000000 ) ) ;
#16762=VERTEX_POINT ( 'NONE', #25891 ) ;
#16807=CIRCLE ( 'NONE', #4934, 15.00000000000000178 ) ;
#16949=CARTESIAN_POINT ( 'NONE',  ( -7.000000000000002665, 19.59999999999999787, 0.000000000000000000 ) ) ;
#16959=ORIENTED_EDGE ( 'NONE', *, *, #17722, .F. ) ;
#16968=VERTEX_POINT ( 'NONE', #17208 ) ;
#17041=EDGE_CURVE ( 'NONE', #16762, #11045, #24127, .T. ) ;
#17054=VERTEX_POINT ( 'NONE', #4272 ) ;
#17085=CARTESIAN_POINT ( 'NONE',  ( -5.991980000000000750, 0.000000000000000000, 0.000000000000000000 ) ) ;
#17098=AXIS2_PLACEMENT_3D ( 'NONE', #2487, #38941, #26086 ) ;
#17112=CARTESIAN_POINT ( 'NONE',  ( -5.991980000000000750, 1.842114939924247430E-15, -14.99999999999999822 ) ) ;
#17125=ORIENTED_EDGE ( 'NONE', *, *, #25333, .F. ) ;
#17146=VERTEX_POINT ( 'NONE', #14786 ) ;
#17208=CARTESIAN_POINT ( 'NONE',  ( -6.599999999999991651, -19.99999999999999289, 2.449293598294706119E-15 ) ) ;
#17234=CARTESIAN_POINT ( 'NONE',  ( 6.600000000000004974, 19.59999999999999787, 0.000000000000000000 ) ) ;
#17252=CARTESIAN_POINT ( 'NONE',  ( 6.200000000000003730, 6.971071669133949438E-15, 0.000000000000000000 ) ) ;
#17396=ORIENTED_EDGE ( 'NONE', *, *, #12143, .F. ) ;
#17399=CARTESIAN_POINT ( 'NONE',  ( -6.004904395537136175, -19.19999999999999574, 2.351321854362917684E-15 ) ) ;
#17537=AXIS2_PLACEMENT_3D ( 'NONE', #26667, #23413, #39934 ) ;
#17565=ORIENTED_EDGE ( 'NONE', *, *, #39768, .F. ) ;
#17603=ADVANCED_FACE ( 'NONE', ( #14288 ), #20027, .T. ) ;
#17722=EDGE_CURVE ( 'NONE', #4034, #21051, #29069, .T. ) ;
#17774=ADVANCED_FACE ( 'NONE', ( #2654 ), #41951, .F. ) ;
#17867=EDGE_LOOP ( 'NONE', ( #38223, #34122, #12802, #19783 ) ) ;
#17992=VECTOR ( 'NONE', #43079, 1000.000000000000000 ) ;
#18110=AXIS2_PLACEMENT_3D ( 'NONE', #11518, #8237, #18312 ) ;
#18204=ORIENTED_EDGE ( 'NONE', *, *, #39768, .T. ) ;
#18220=EDGE_CURVE ( 'NONE', #5342, #35630, #35338, .T. ) ;
#18231=AXIS2_PLACEMENT_3D ( 'NONE', #42921, #39005, #6071 ) ;
#18283=AXIS2_PLACEMENT_3D ( 'NONE', #30194, #30415, #33244 ) ;
#18312=DIRECTION ( 'NONE',  ( 0.000000000000000000, -1.000000000000000000, 1.224646799147353207E-16 ) ) ;
#18353=VECTOR ( 'NONE', #42721, 1000.000000000000000 ) ;
#18356=CARTESIAN_POINT ( 'NONE',  ( -25.39999999999999147, 1.836970198721029589E-15, -15.00000000000000000 ) ) ;
#18438=CARTESIAN_POINT ( 'NONE',  ( -6.004904395537136175, 19.19999999999999574, 0.000000000000000000 ) ) ;
#18477=ORIENTED_EDGE ( 'NONE', *, *, #10315, .F. ) ;
#18501=CIRCLE ( 'NONE', #42810, 19.19999999999999574 ) ;
#18604=UNCERTAINTY_MEASURE_WITH_UNIT (LENGTH_MEASURE( 1.000000000000000082E-05 ), #12510, 'distance_accuracy_value', 'NONE');
#18623=MECHANICAL_DESIGN_GEOMETRIC_PRESENTATION_REPRESENTATION('',(#40113),#9497);
#18705=DIRECTION ( 'NONE',  ( -1.000000000000000000, 0.000000000000000000, 0.000000000000000000 ) ) ;
#18710=ADVANCED_FACE ( 'NONE', ( #9123 ), #15275, .T. ) ;
#18744=EDGE_LOOP ( 'NONE', ( #4005, #21586, #16483, #23849 ) ) ;
#18795=AXIS2_PLACEMENT_3D ( 'NONE', #8391, #18705, #25034 ) ;
#18819=EDGE_CURVE ( 'NONE', #37013, #39320, #9645, .T. ) ;
#18825=CARTESIAN_POINT ( 'NONE',  ( -31.75000000000000000, -18.77999999999999048, 2.299886688798728323E-15 ) ) ;
#18885=EDGE_CURVE ( 'NONE', #20227, #31507, #13125, .T. ) ;
#19206=AXIS2_PLACEMENT_3D ( 'NONE', #1376, #5082, #14725 ) ;
#19229=VERTEX_POINT ( 'NONE', #19520 ) ;
#19321=CARTESIAN_POINT ( 'NONE',  ( 6.075999999999997847, 0.000000000000000000, 0.000000000000000000 ) ) ;
#19336=ORIENTED_EDGE ( 'NONE', *, *, #13740, .F. ) ;
#19430=DIRECTION ( 'NONE',  ( 1.000000000000000000, 1.836909530733573776E-16, 0.000000000000000000 ) ) ;
#19443=FACE_OUTER_BOUND ( 'NONE', #14648, .T. ) ;
#19464=EDGE_CURVE ( 'NONE', #17146, #17054, #2032, .T. ) ;
#19476=DIRECTION ( 'NONE',  ( 0.000000000000000000, 0.000000000000000000, -1.000000000000000000 ) ) ;
#19484=AXIS2_PLACEMENT_3D ( 'NONE', #24632, #10866, #40719 ) ;
#19517=ORIENTED_EDGE ( 'NONE', *, *, #33327, .T. ) ;
#19520=CARTESIAN_POINT ( 'NONE',  ( 6.004904395537136175, 19.19999999999999574, 0.000000000000000000 ) ) ;
#19526=ORIENTED_EDGE ( 'NONE', *, *, #5494, .T. ) ;
#19620=( NAMED_UNIT ( * ) SI_UNIT ( $, .STERADIAN. ) SOLID_ANGLE_UNIT ( ) );
#19715=CARTESIAN_POINT ( 'NONE',  ( -6.075999999999999623, 0.000000000000000000, 15.08402000000000065 ) ) ;
#19721=FACE_OUTER_BOUND ( 'NONE', #35648, .T. ) ;
#19738=FACE_OUTER_BOUND ( 'NONE', #12457, .T. ) ;
#19743=EDGE_LOOP ( 'NONE', ( #11969, #7126 ) ) ;
#19757=ORIENTED_EDGE ( 'NONE', *, *, #28082, .F. ) ;
#19758=CARTESIAN_POINT ( 'NONE',  ( 6.200000000000007283, -19.19999999999998508, 2.351321854362917290E-15 ) ) ;
#19771=DIRECTION ( 'NONE',  ( 1.000000000000000000, 1.836909530733573776E-16, 0.000000000000000000 ) ) ;
#19783=ORIENTED_EDGE ( 'NONE', *, *, #21279, .F. ) ;
#19798=ORIENTED_EDGE ( 'NONE', *, *, #9475, .T. ) ;
#19894=DIRECTION ( 'NONE',  ( -3.614007241618348771E-16, 1.000000000000000000, 0.000000000000000000 ) ) ;
#19945=DIRECTION ( 'NONE',  ( 0.000000000000000000, 1.000000000000000000, 0.000000000000000000 ) ) ;
#20010=DIRECTION ( 'NONE',  ( -1.847415842360817977E-16, 1.000000000000000000, 0.000000000000000000 ) ) ;
#20027=TOROIDAL_SURFACE ( 'NONE', #40864, 15.08402000000000065, 0.08402000000000148239 ) ;
#20038=DIRECTION ( 'NONE',  ( 1.000000000000000000, 1.836909530733573776E-16, 0.000000000000000000 ) ) ;
#20151=DIRECTION ( 'NONE',  ( -1.000000000000000000, 0.000000000000000000, 0.000000000000000000 ) ) ;
#20166=DIRECTION ( 'NONE',  ( 0.000000000000000000, 0.000000000000000000, 1.000000000000000000 ) ) ;
#20174=CARTESIAN_POINT ( 'NONE',  ( -6.199999999999993960, -19.19999999999999218, 2.351321854362917684E-15 ) ) ;
#20227=VERTEX_POINT ( 'NONE', #33342 ) ;
#20384=DIRECTION ( 'NONE',  ( 0.000000000000000000, 1.000000000000000000, 1.224646799147353207E-16 ) ) ;
#20411=AXIS2_PLACEMENT_3D ( 'NONE', #17252, #27467, #30744 ) ;
#20418=CIRCLE ( 'NONE', #1562, 0.4000000000000001887 ) ;
#20470=ADVANCED_FACE ( 'NONE', ( #27445, #7792 ), #1243, .F. ) ;
#20500=EDGE_CURVE ( 'NONE', #40959, #24696, #10391, .T. ) ;
#20578=EDGE_CURVE ( 'NONE', #42589, #13405, #11098, .T. ) ;
#20621=EDGE_CURVE ( 'NONE', #16491, #16968, #43105, .T. ) ;
#20661=EDGE_CURVE ( 'NONE', #28909, #16968, #34779, .T. ) ;
#20692=VECTOR ( 'NONE', #590, 1000.000000000000000 ) ;
#20736=FACE_OUTER_BOUND ( 'NONE', #1591, .T. ) ;
#20785=CARTESIAN_POINT ( 'NONE',  ( -31.75000000000000711, 19.19999999999999574, 0.000000000000000000 ) ) ;
#20856=CARTESIAN_POINT ( 'NONE',  ( -6.999999999999999112, 4.546351088565595293E-15, 0.000000000000000000 ) ) ;
#20921=CARTESIAN_POINT ( 'NONE',  ( 6.600000000000001421, 7.044548050363292547E-15, 0.000000000000000000 ) ) ;
#20931=EDGE_CURVE ( 'NONE', #31507, #12750, #40888, .T. ) ;
#20953=DIRECTION ( 'NONE',  ( 1.000000000000000000, 1.836909530733573776E-16, 0.000000000000000000 ) ) ;
#21051=VERTEX_POINT ( 'NONE', #19715 ) ;
#21072=DIRECTION ( 'NONE',  ( -1.847415842360817484E-16, 1.000000000000000000, 0.000000000000000000 ) ) ;
#21094=TOROIDAL_SURFACE ( 'NONE', #35661, 19.11697999999999809, 0.08401999999999931745 ) ;
#21121=EDGE_CURVE ( 'NONE', #4294, #29681, #35876, .T. ) ;
#21160=VERTEX_POINT ( 'NONE', #10725 ) ;
#21279=EDGE_CURVE ( 'NONE', #16491, #16762, #22676, .T. ) ;
#21400=ORIENTED_EDGE ( 'NONE', *, *, #23157, .F. ) ;
#21416=ORIENTED_EDGE ( 'NONE', *, *, #13740, .T. ) ;
#21466=CARTESIAN_POINT ( 'NONE',  ( -6.199999999999997513, 4.693303851024319376E-15, 0.000000000000000000 ) ) ;
#21507=DIRECTION ( 'NONE',  ( -1.000000000000000000, 0.000000000000000000, 0.000000000000000000 ) ) ;
#21543=AXIS2_PLACEMENT_3D ( 'NONE', #22269, #31842, #1710 ) ;
#21545=CIRCLE ( 'NONE', #31249, 18.77999999999999403 ) ;
#21586=ORIENTED_EDGE ( 'NONE', *, *, #17722, .T. ) ;
#21616=ORIENTED_EDGE ( 'NONE', *, *, #13001, .F. ) ;
#21725=EDGE_CURVE ( 'NONE', #30619, #28909, #26056, .T. ) ;
#21770=ORIENTED_EDGE ( 'NONE', *, *, #31173, .F. ) ;
#21829=ORIENTED_EDGE ( 'NONE', *, *, #23157, .T. ) ;
#21918=DIRECTION ( 'NONE',  ( 0.000000000000000000, 0.000000000000000000, 1.000000000000000000 ) ) ;
#22067=ORIENTED_EDGE ( 'NONE', *, *, #3209, .F. ) ;
#22075=CARTESIAN_POINT ( 'NONE',  ( -5.991980000000000750, 0.000000000000000000, 19.11697999999999809 ) ) ;
#22156=AXIS2_PLACEMENT_3D ( 'NONE', #41761, #38059, #28701 ) ;
#22217=AXIS2_PLACEMENT_3D ( 'NONE', #5205, #24902, #38156 ) ;
#22248=ORIENTED_EDGE ( 'NONE', *, *, #28900, .T. ) ;
#22260=CARTESIAN_POINT ( 'NONE',  ( -6.199999999999997513, 4.693303851024319376E-15, 0.000000000000000000 ) ) ;
#22269=CARTESIAN_POINT ( 'NONE',  ( -5.991980000000000750, 0.000000000000000000, 0.000000000000000000 ) ) ;
#22348=SHAPE_REPRESENTATION_RELATIONSHIP ( 'NONE' , 'NONE' ,  #7878, #10920 ) ;
#22435=DIRECTION ( 'NONE',  ( -1.847415842360817977E-16, 1.000000000000000000, 0.000000000000000000 ) ) ;
#22483=FACE_OUTER_BOUND ( 'NONE', #30614, .T. ) ;
#22538=DIRECTION ( 'NONE',  ( -1.000000000000000000, 0.000000000000000000, 0.000000000000000000 ) ) ;
#22635=ORIENTED_EDGE ( 'NONE', *, *, #9342, .T. ) ;
#22641=CARTESIAN_POINT ( 'NONE',  ( 6.600000000000012079, -19.59999999999998721, 2.400307726328811507E-15 ) ) ;
#22650=CIRCLE ( 'NONE', #2368, 18.77999999999999403 ) ;
#22676=LINE ( 'NONE', #12419, #31051 ) ;
#22784=EDGE_CURVE ( 'NONE', #17146, #39595, #42864, .T. ) ;
#22789=DIRECTION ( 'NONE',  ( 0.000000000000000000, 1.000000000000000000, 0.000000000000000000 ) ) ;
#22814=ORIENTED_EDGE ( 'NONE', *, *, #18885, .T. ) ;
#22848=ORIENTED_EDGE ( 'NONE', *, *, #3376, .T. ) ;
#22875=FACE_OUTER_BOUND ( 'NONE', #37164, .T. ) ;
#22914=DIRECTION ( 'NONE',  ( -1.847415842360817484E-16, 1.000000000000000000, 0.000000000000000000 ) ) ;
#22942=CARTESIAN_POINT ( 'NONE',  ( 6.004904395537136175, 2.351321854362917684E-15, -19.19999999999999574 ) ) ;
#22944=DIRECTION ( 'NONE',  ( 1.000000000000000000, 1.836909530733573776E-16, 0.000000000000000000 ) ) ;
#22947=ORIENTED_EDGE ( 'NONE', *, *, #21279, .T. ) ;
#22955=AXIS2_PLACEMENT_3D ( 'NONE', #5801, #5597, #41812 ) ;
#22979=ORIENTED_EDGE ( 'NONE', *, *, #41900, .T. ) ;
#23027=ORIENTED_EDGE ( 'NONE', *, *, #20578, .F. ) ;
#23136=ORIENTED_EDGE ( 'NONE', *, *, #37138, .T. ) ;
#23157=EDGE_CURVE ( 'NONE', #41075, #36558, #42148, .T. ) ;
#23326=ORIENTED_EDGE ( 'NONE', *, *, #23485, .T. ) ;
#23411=CIRCLE ( 'NONE', #42859, 0.08401999999999888724 ) ;
#23413=DIRECTION ( 'NONE',  ( -1.000000000000000000, 0.000000000000000000, 0.000000000000000000 ) ) ;
#23440=AXIS2_PLACEMENT_3D ( 'NONE', #22075, #15317, #15726 ) ;
#23485=EDGE_CURVE ( 'NONE', #21051, #4034, #16473, .T. ) ;
#23607=CARTESIAN_POINT ( 'NONE',  ( -5.991980000000000750, 0.000000000000000000, 15.08402000000000065 ) ) ;
#23634=CARTESIAN_POINT ( 'NONE',  ( -5.991980000000000750, 0.000000000000000000, 0.000000000000000000 ) ) ;
#23680=DIRECTION ( 'NONE',  ( -1.770125995894701695E-16, 1.000000000000000000, 0.000000000000000000 ) ) ;
#23701=EDGE_CURVE ( 'NONE', #16968, #11045, #26799, .T. ) ;
#23821=CARTESIAN_POINT ( 'NONE',  ( -25.39999999999999147, 0.000000000000000000, 0.000000000000000000 ) ) ;
#23830=CARTESIAN_POINT ( 'NONE',  ( -31.75000000000000000, 0.000000000000000000, 0.000000000000000000 ) ) ;
#23846=ORIENTED_EDGE ( 'NONE', *, *, #32720, .F. ) ;
#23849=ORIENTED_EDGE ( 'NONE', *, *, #38942, .F. ) ;
#23875=CIRCLE ( 'NONE', #2207, 19.59999999999999432 ) ;
#23899=DIRECTION ( 'NONE',  ( 0.000000000000000000, 0.000000000000000000, -1.000000000000000000 ) ) ;
#23902=CARTESIAN_POINT ( 'NONE',  ( -6.200000000000003730, 19.19999999999999929, 0.000000000000000000 ) ) ;
#23952=CIRCLE ( 'NONE', #7180, 19.19999999999999574 ) ;
#24046=CARTESIAN_POINT ( 'NONE',  ( -31.75000000000000000, 0.000000000000000000, 0.000000000000000000 ) ) ;
#24122=DIRECTION ( 'NONE',  ( 0.000000000000000000, 0.000000000000000000, 1.000000000000000000 ) ) ;
#24127=CIRCLE ( 'NONE', #29685, 19.99999999999999289 ) ;
#24165=AXIS2_PLACEMENT_3D ( 'NONE', #26462, #9860, #32778 ) ;
#24217=CARTESIAN_POINT ( 'NONE',  ( -5.991980000000000750, 0.000000000000000000, 0.000000000000000000 ) ) ;
#24237=VECTOR ( 'NONE', #28093, 1000.000000000000000 ) ;
#24264=DIRECTION ( 'NONE',  ( 0.000000000000000000, 0.000000000000000000, 1.000000000000000000 ) ) ;
#24332=EDGE_LOOP ( 'NONE', ( #12624, #22979, #14432, #7974 ) ) ;
#24334=CIRCLE ( 'NONE', #10267, 0.4000000000000001887 ) ;
#24369=CARTESIAN_POINT ( 'NONE',  ( -31.75000000000000000, -18.77999999999999403, 2.299886688798728717E-15 ) ) ;
#24488=DIRECTION ( 'NONE',  ( -3.614007241618348771E-16, 1.000000000000000000, 0.000000000000000000 ) ) ;
#24577=EDGE_LOOP ( 'NONE', ( #39747, #15785, #10784, #16603 ) ) ;
#24590=AXIS2_PLACEMENT_3D ( 'NONE', #9594, #13104, #6509 ) ;
#24625=AXIS2_PLACEMENT_3D ( 'NONE', #32905, #19430, #6491 ) ;
#24632=CARTESIAN_POINT ( 'NONE',  ( 6.075999999999990742, 19.11698000000008335, 0.000000000000000000 ) ) ;
#24696=VERTEX_POINT ( 'NONE', #36437 ) ;
#24782=DIRECTION ( 'NONE',  ( -1.770125995894701942E-16, 1.000000000000000000, 0.000000000000000000 ) ) ;
#24802=EDGE_CURVE ( 'NONE', #9440, #36558, #40811, .T. ) ;
#24832=AXIS2_PLACEMENT_3D ( 'NONE', #21466, #4601, #14026 ) ;
#24845=ORIENTED_EDGE ( 'NONE', *, *, #26157, .T. ) ;
#24886=DIRECTION ( 'NONE',  ( -3.614007241618348771E-16, 1.000000000000000000, 0.000000000000000000 ) ) ;
#24902=DIRECTION ( 'NONE',  ( 1.000000000000000000, 0.000000000000000000, 0.000000000000000000 ) ) ;
#24904=CIRCLE ( 'NONE', #6038, 18.77999999999999048 ) ;
#25026=ORIENTED_EDGE ( 'NONE', *, *, #1706, .T. ) ;
#25034=DIRECTION ( 'NONE',  ( 0.000000000000000000, 0.000000000000000000, 1.000000000000000000 ) ) ;
#25076=EDGE_LOOP ( 'NONE', ( #10069, #14459 ) ) ;
#25232=EDGE_CURVE ( 'NONE', #13405, #42589, #15520, .T. ) ;
#25333=EDGE_CURVE ( 'NONE', #35630, #5342, #27329, .T. ) ;
#25454=ORIENTED_EDGE ( 'NONE', *, *, #5762, .T. ) ;
#25581=ADVANCED_FACE ( 'NONE', ( #11542 ), #8260, .F. ) ;
#25624=EDGE_LOOP ( 'NONE', ( #13180, #22848 ) ) ;
#25637=DIRECTION ( 'NONE',  ( -1.000000000000000000, 0.000000000000000000, 0.000000000000000000 ) ) ;
#25738=DIRECTION ( 'NONE',  ( 1.000000000000000000, 1.836909530733573776E-16, 0.000000000000000000 ) ) ;
#25752=FACE_BOUND ( 'NONE', #13198, .T. ) ;
#25790=DIRECTION ( 'NONE',  ( 1.000000000000000000, 1.836909530733573776E-16, 0.000000000000000000 ) ) ;
#25844=ORIENTED_EDGE ( 'NONE', *, *, #23485, .F. ) ;
#25863=AXIS2_PLACEMENT_3D ( 'NONE', #24217, #14818, #27691 ) ;
#25891=CARTESIAN_POINT ( 'NONE',  ( 6.599999999999997868, 20.00000000000000000, 0.000000000000000000 ) ) ;
#25922=DIRECTION ( 'NONE',  ( 1.000000000000000000, 1.836909530733573776E-16, 0.000000000000000000 ) ) ;
#25943=CIRCLE ( 'NONE', #12699, 19.19999999999999574 ) ;
#25955=CARTESIAN_POINT ( 'NONE',  ( -6.075999999999997847, 0.000000000000000000, 0.000000000000000000 ) ) ;
#26056=CIRCLE ( 'NONE', #33689, 19.59999999999999432 ) ;
#26058=DIRECTION ( 'NONE',  ( -1.000000000000000000, 0.000000000000000000, 0.000000000000000000 ) ) ;
#26086=DIRECTION ( 'NONE',  ( -1.836909530733573776E-16, 1.000000000000000000, 0.000000000000000000 ) ) ;
#26148=VECTOR ( 'NONE', #26960, 1000.000000000000000 ) ;
#26157=EDGE_CURVE ( 'NONE', #41075, #5519, #23952, .T. ) ;
#26275=DIRECTION ( 'NONE',  ( 0.000000000000000000, 0.000000000000000000, 1.000000000000000000 ) ) ;
#26366=CIRCLE ( 'NONE', #14545, 18.77999999999999403 ) ;
#26439=DIRECTION ( 'NONE',  ( -1.000000000000000000, 0.000000000000000000, 0.000000000000000000 ) ) ;
#26462=CARTESIAN_POINT ( 'NONE',  ( -31.75000000000000000, 0.000000000000000000, 0.000000000000000000 ) ) ;
#26483=CARTESIAN_POINT ( 'NONE',  ( -6.004904395537136175, 0.000000000000000000, 19.19999999999999574 ) ) ;
#26545=DIRECTION ( 'NONE',  ( 0.000000000000000000, -1.000000000000000000, 0.000000000000000000 ) ) ;
#26547=CARTESIAN_POINT ( 'NONE',  ( -31.75000000000000000, 0.000000000000000000, 0.000000000000000000 ) ) ;
#26667=CARTESIAN_POINT ( 'NONE',  ( 5.991980000000000750, 0.000000000000000000, 0.000000000000000000 ) ) ;
#26799=LINE ( 'NONE', #30518, #20692 ) ;
#26960=DIRECTION ( 'NONE',  ( -1.000000000000000000, 0.000000000000000000, 0.000000000000000000 ) ) ;
#26967=CARTESIAN_POINT ( 'NONE',  ( -6.075999999999997847, 2.346238345499656945E-15, -19.11697999999999809 ) ) ;
#27023=ORIENTED_EDGE ( 'NONE', *, *, #13345, .F. ) ;
#27089=ORIENTED_EDGE ( 'NONE', *, *, #36751, .T. ) ;
#27128=ORIENTED_EDGE ( 'NONE', *, *, #18220, .F. ) ;
#27191=AXIS2_PLACEMENT_3D ( 'NONE', #8129, #41051, #34306 ) ;
#27209=ORIENTED_EDGE ( 'NONE', *, *, #17041, .T. ) ;
#27212=ORIENTED_EDGE ( 'NONE', *, *, #14582, .F. ) ;
#27280=EDGE_CURVE ( 'NONE', #12750, #40931, #22650, .T. ) ;
#27284=DIRECTION ( 'NONE',  ( 0.000000000000000000, 0.000000000000000000, -1.000000000000000000 ) ) ;
#27329=CIRCLE ( 'NONE', #20411, 19.19999999999999218 ) ;
#27435=EDGE_LOOP ( 'NONE', ( #27843, #21829, #14453, #23846, #2994 ) ) ;
#27445=FACE_OUTER_BOUND ( 'NONE', #42596, .T. ) ;
#27467=DIRECTION ( 'NONE',  ( 1.000000000000000000, 1.836909530733573776E-16, 0.000000000000000000 ) ) ;
#27489=CYLINDRICAL_SURFACE ( 'NONE', #5195, 18.77999999999999048 ) ;
#27652=ADVANCED_FACE ( 'NONE', ( #6213 ), #39336, .T. ) ;
#27664=LINE ( 'NONE', #31354, #24237 ) ;
#27691=DIRECTION ( 'NONE',  ( 0.000000000000000000, 0.000000000000000000, 1.000000000000000000 ) ) ;
#27843=ORIENTED_EDGE ( 'NONE', *, *, #26157, .F. ) ;
#27848=ADVANCED_FACE ( 'NONE', ( #37387, #3763 ), #10569, .T. ) ;
#27884=AXIS2_PLACEMENT_3D ( 'NONE', #16304, #26545, #33302 ) ;
#27897=APPLICATION_CONTEXT ( 'automotive_design' ) ;
#28082=EDGE_CURVE ( 'NONE', #2217, #1510, #34532, .T. ) ;
#28093=DIRECTION ( 'NONE',  ( 1.000000000000000000, 1.836909530733573776E-16, 0.000000000000000000 ) ) ;
#28214=ORIENTED_EDGE ( 'NONE', *, *, #38394, .T. ) ;
#28329=DIRECTION ( 'NONE',  ( 1.000000000000000000, 1.836909530733573776E-16, 0.000000000000000000 ) ) ;
#28373=CARTESIAN_POINT ( 'NONE',  ( -6.599999999999994316, 4.619827469794975478E-15, 0.000000000000000000 ) ) ;
#28464=SURFACE_STYLE_FILL_AREA ( #12297 ) ;
#28532=EDGE_CURVE ( 'NONE', #16968, #16491, #35950, .T. ) ;
#28662=MANIFOLD_SOLID_BREP ( 'RollersSimplified', #11473 ) ;
#28701=DIRECTION ( 'NONE',  ( 0.000000000000000000, -1.224646799147359124E-16, 1.000000000000000000 ) ) ;
#28753=ORIENTED_EDGE ( 'NONE', *, *, #22784, .F. ) ;
#28838=COLOUR_RGB ( '', 0.40784314, 0.44705882, 0.49803922) ;
#28900=EDGE_CURVE ( 'NONE', #4294, #5519, #31566, .T. ) ;
#28909=VERTEX_POINT ( 'NONE', #11950 ) ;
#28952=AXIS2_PLACEMENT_3D ( 'NONE', #23902, #19771, #33035 ) ;
#28953=CARTESIAN_POINT ( 'NONE',  ( -6.999999999999992006, 18.77999999999999758, 0.000000000000000000 ) ) ;
#28976=AXIS2_PLACEMENT_3D ( 'NONE', #3272, #26439, #29938 ) ;
#28986=EDGE_CURVE ( 'NONE', #24696, #40959, #24904, .T. ) ;
#29047=CARTESIAN_POINT ( 'NONE',  ( -6.075999999999999623, 1.847259681127465666E-15, -15.08402000000000065 ) ) ;
#29069=CIRCLE ( 'NONE', #32533, 15.08402000000000065 ) ;
#29167=ORIENTED_EDGE ( 'NONE', *, *, #20931, .F. ) ;
#29374=EDGE_LOOP ( 'NONE', ( #6537, #15665 ) ) ;
#29444=ORIENTED_EDGE ( 'NONE', *, *, #14582, .T. ) ;
#29498=CARTESIAN_POINT ( 'NONE',  ( -6.075999999999997847, 0.000000000000000000, 0.000000000000000000 ) ) ;
#29567=DIRECTION ( 'NONE',  ( 0.000000000000000000, 0.000000000000000000, 1.000000000000000000 ) ) ;
#29681=VERTEX_POINT ( 'NONE', #20174 ) ;
#29685=AXIS2_PLACEMENT_3D ( 'NONE', #20921, #41579, #35035 ) ;
#29700=CARTESIAN_POINT ( 'NONE',  ( -6.199999999999997513, 4.693303851024319376E-15, 0.000000000000000000 ) ) ;
#29809=ORIENTED_EDGE ( 'NONE', *, *, #15966, .F. ) ;
#29856=DIRECTION ( 'NONE',  ( 1.000000000000000000, 1.836909530733573776E-16, 0.000000000000000000 ) ) ;
#29885=EDGE_CURVE ( 'NONE', #31507, #20227, #26366, .T. ) ;
#29938=DIRECTION ( 'NONE',  ( 0.000000000000000000, 0.000000000000000000, 1.000000000000000000 ) ) ;
#30064=ADVANCED_FACE ( 'NONE', ( #4123 ), #10256, .F. ) ;
#30083=EDGE_CURVE ( 'NONE', #21051, #39595, #9623, .T. ) ;
#30194=CARTESIAN_POINT ( 'NONE',  ( 6.075999999999997847, 0.000000000000000000, 0.000000000000000000 ) ) ;
#30253=DIRECTION ( 'NONE',  ( 0.000000000000000000, 0.000000000000000000, -1.000000000000000000 ) ) ;
#30370=FACE_OUTER_BOUND ( 'NONE', #12972, .T. ) ;
#30390=EDGE_LOOP ( 'NONE', ( #11984, #9233, #27089, #41048, #36719 ) ) ;
#30415=DIRECTION ( 'NONE',  ( -1.000000000000000000, 0.000000000000000000, 0.000000000000000000 ) ) ;
#30428=FACE_OUTER_BOUND ( 'NONE', #16455, .T. ) ;
#30431=EDGE_CURVE ( 'NONE', #11045, #2217, #10239, .T. ) ;
#30518=CARTESIAN_POINT ( 'NONE',  ( -31.74999999999999289, -19.99999999999999645, 2.449293598294706119E-15 ) ) ;
#30543=AXIS2_PLACEMENT_3D ( 'NONE', #13986, #13130, #19894 ) ;
#30603=EDGE_CURVE ( 'NONE', #21160, #5342, #534, .T. ) ;
#30614=EDGE_LOOP ( 'NONE', ( #19517, #14192 ) ) ;
#30616=AXIS2_PLACEMENT_3D ( 'NONE', #9080, #2292, #15653 ) ;
#30619=VERTEX_POINT ( 'NONE', #16949 ) ;
#30640=DIRECTION ( 'NONE',  ( -1.000000000000000000, 0.000000000000000000, 0.000000000000000000 ) ) ;
#30689=EDGE_CURVE ( 'NONE', #4034, #15674, #38147, .T. ) ;
#30696=CARTESIAN_POINT ( 'NONE',  ( 6.999999999999995559, 18.77999999999999758, 0.000000000000000000 ) ) ;
#30744=DIRECTION ( 'NONE',  ( -1.807003620809174878E-16, 1.000000000000000000, 0.000000000000000000 ) ) ;
#30802=DIRECTION ( 'NONE',  ( 0.000000000000000000, 0.000000000000000000, 1.000000000000000000 ) ) ;
#31021=CARTESIAN_POINT ( 'NONE',  ( 5.991979999999993645, 0.000000000000000000, 0.000000000000000000 ) ) ;
#31028=AXIS2_PLACEMENT_3D ( 'NONE', #7028, #20384, #13611 ) ;
#31051=VECTOR ( 'NONE', #25738, 1000.000000000000000 ) ;
#31052=CARTESIAN_POINT ( 'NONE',  ( 6.075999999999998735, 1.847259681127465666E-15, -15.08402000000000065 ) ) ;
#31061=AXIS2_PLACEMENT_3D ( 'NONE', #31947, #2027, #24782 ) ;
#31173=EDGE_CURVE ( 'NONE', #19229, #35630, #31218, .T. ) ;
#31181=CARTESIAN_POINT ( 'NONE',  ( 7.000000000000009770, -19.59999999999998721, 2.424800662311758221E-15 ) ) ;
#31218=LINE ( 'NONE', #20785, #9295 ) ;
#31247=AXIS2_PLACEMENT_3D ( 'NONE', #32681, #10191, #22914 ) ;
#31249=AXIS2_PLACEMENT_3D ( 'NONE', #10774, #38241, #21072 ) ;
#31265=DIRECTION ( 'NONE',  ( 1.836909530733573776E-16, -1.000000000000000000, 0.000000000000000000 ) ) ;
#31283=CARTESIAN_POINT ( 'NONE',  ( 5.991979999999993645, 0.000000000000000000, 0.000000000000000000 ) ) ;
#31330=TOROIDAL_SURFACE ( 'NONE', #25863, 19.11697999999999809, 0.08401999999999801294 ) ;
#31354=CARTESIAN_POINT ( 'NONE',  ( -31.74999999999999289, -19.19999999999999574, 2.351321854362917684E-15 ) ) ;
#31507=VERTEX_POINT ( 'NONE', #2576 ) ;
#31516=ORIENTED_EDGE ( 'NONE', *, *, #23701, .F. ) ;
#31546=EDGE_LOOP ( 'NONE', ( #25026, #42269, #37842, #9100, #21770 ) ) ;
#31566=LINE ( 'NONE', #15012, #15810 ) ;
#31666=CARTESIAN_POINT ( 'NONE',  ( 6.200000000000003730, 6.971071669133949438E-15, 0.000000000000000000 ) ) ;
#31815=CARTESIAN_POINT ( 'NONE',  ( 6.004904395537136175, 0.000000000000000000, 19.19999999999999574 ) ) ;
#31842=DIRECTION ( 'NONE',  ( -1.000000000000000000, 0.000000000000000000, 0.000000000000000000 ) ) ;
#31895=AXIS2_PLACEMENT_3D ( 'NONE', #23821, #33818, #24264 ) ;
#31947=CARTESIAN_POINT ( 'NONE',  ( 7.000000000000006217, 7.118024431592600946E-15, 0.000000000000000000 ) ) ;
#31985=CIRCLE ( 'NONE', #18795, 19.19999999999999574 ) ;
#32143=ORIENTED_EDGE ( 'NONE', *, *, #30689, .T. ) ;
#32314=EDGE_LOOP ( 'NONE', ( #6482, #1781, #13392, #29809 ) ) ;
#32405=EDGE_CURVE ( 'NONE', #17146, #9453, #15070, .T. ) ;
#32497=PRODUCT_DEFINITION_CONTEXT ( 'detailed design', #27897, 'design' ) ;
#32533=AXIS2_PLACEMENT_3D ( 'NONE', #11886, #25637, #38460 ) ;
#32551=CARTESIAN_POINT ( 'NONE',  ( -6.600000000000001421, 3.469446951953649688E-15, 0.000000000000000000 ) ) ;
#32588=ADVANCED_FACE ( 'NONE', ( #41439 ), #40571, .F. ) ;
#32631=EDGE_LOOP ( 'NONE', ( #3745, #35846 ) ) ;
#32681=CARTESIAN_POINT ( 'NONE',  ( -6.999999999999999112, 4.546351088565595293E-15, 0.000000000000000000 ) ) ;
#32689=AXIS2_PLACEMENT_3D ( 'NONE', #33865, #39536, #36259 ) ;
#32720=EDGE_CURVE ( 'NONE', #37013, #9440, #5994, .T. ) ;
#32762=CIRCLE ( 'NONE', #38346, 14.99999999999999822 ) ;
#32778=DIRECTION ( 'NONE',  ( -3.614007241618348771E-16, 1.000000000000000000, 0.000000000000000000 ) ) ;
#32854=CARTESIAN_POINT ( 'NONE',  ( -31.75000000000000000, 0.000000000000000000, 0.000000000000000000 ) ) ;
#32905=CARTESIAN_POINT ( 'NONE',  ( 6.600000000000001421, 7.044548050363292547E-15, 0.000000000000000000 ) ) ;
#32995=VERTEX_POINT ( 'NONE', #22942 ) ;
#33000=PLANE ( 'NONE',  #11775 ) ;
#33035=DIRECTION ( 'NONE',  ( -1.836909530733573776E-16, 1.000000000000000000, 0.000000000000000000 ) ) ;
#33062=CYLINDRICAL_SURFACE ( 'NONE', #9256, 19.99999999999999645 ) ;
#33070=CARTESIAN_POINT ( 'NONE',  ( 6.600000000000004974, -19.99999999999998579, 2.449293598294705724E-15 ) ) ;
#33082=ADVANCED_FACE ( 'NONE', ( #20736 ), #3163, .T. ) ;
#33102=SURFACE_STYLE_USAGE ( .BOTH. , #35717 ) ;
#33244=DIRECTION ( 'NONE',  ( 0.000000000000000000, 0.000000000000000000, 1.000000000000000000 ) ) ;
#33302=DIRECTION ( 'NONE',  ( 0.000000000000000000, 0.000000000000000000, -1.000000000000000000 ) ) ;
#33303=DIRECTION ( 'NONE',  ( 0.000000000000000000, 1.000000000000000000, 0.000000000000000000 ) ) ;
#33327=EDGE_CURVE ( 'NONE', #1510, #2217, #38074, .T. ) ;
#33342=CARTESIAN_POINT ( 'NONE',  ( -7.000000000000002665, 18.77999999999999758, 0.000000000000000000 ) ) ;
#33369=AXIS2_PLACEMENT_3D ( 'NONE', #19321, #26058, #26275 ) ;
#33481=LINE ( 'NONE', #39795, #17992 ) ;
#33513=EDGE_LOOP ( 'NONE', ( #21400, #12688, #1153, #2616, #35344 ) ) ;
#33551=CARTESIAN_POINT ( 'NONE',  ( -6.075999999999997847, 0.000000000000000000, 19.11697999999999809 ) ) ;
#33661=EDGE_LOOP ( 'NONE', ( #29167, #34962, #2680, #19526 ) ) ;
#33679=ORIENTED_EDGE ( 'NONE', *, *, #21121, .F. ) ;
#33689=AXIS2_PLACEMENT_3D ( 'NONE', #8969, #25790, #39050 ) ;
#33818=DIRECTION ( 'NONE',  ( -1.000000000000000000, 0.000000000000000000, 0.000000000000000000 ) ) ;
#33843=CIRCLE ( 'NONE', #10168, 19.11697999999999809 ) ;
#33865=CARTESIAN_POINT ( 'NONE',  ( 5.991980000000000750, 0.000000000000000000, 15.08402000000000065 ) ) ;
#33922=AXIS2_PLACEMENT_3D ( 'NONE', #13631, #30640, #918 ) ;
#33947=ORIENTED_EDGE ( 'NONE', *, *, #18819, .T. ) ;
#34023=CARTESIAN_POINT ( 'NONE',  ( -31.75000000000000000, 0.000000000000000000, 0.000000000000000000 ) ) ;
#34049=DIRECTION ( 'NONE',  ( -3.469446951953614682E-16, 1.000000000000000000, 0.000000000000000000 ) ) ;
#34105=DIRECTION ( 'NONE',  ( 1.000000000000000000, 1.836909530733573776E-16, 0.000000000000000000 ) ) ;
#34112=( NAMED_UNIT ( * ) SI_UNIT ( $, .STERADIAN. ) SOLID_ANGLE_UNIT ( ) );
#34122=ORIENTED_EDGE ( 'NONE', *, *, #23701, .T. ) ;
#34262=TOROIDAL_SURFACE ( 'NONE', #15492, 19.59999999999999076, 0.4000000000000001887 ) ;
#34290=ORIENTED_EDGE ( 'NONE', *, *, #19464, .T. ) ;
#34306=DIRECTION ( 'NONE',  ( 0.000000000000000000, 0.000000000000000000, 1.000000000000000000 ) ) ;
#34532=CIRCLE ( 'NONE', #31061, 19.59999999999999076 ) ;
#34654=ADVANCED_FACE ( 'NONE', ( #39851 ), #351, .F. ) ;
#34706=PRODUCT_CONTEXT ( 'NONE', #37852, 'mechanical' ) ;
#34779=CIRCLE ( 'NONE', #18110, 0.4000000000000010214 ) ;
#34834=CARTESIAN_POINT ( 'NONE',  ( 7.000000000000002665, -18.77999999999998337, 2.299886688798728323E-15 ) ) ;
#34883=LINE ( 'NONE', #18356, #1731 ) ;
#34927=AXIS2_PLACEMENT_3D ( 'NONE', #2830, #38865, #16194 ) ;
#34962=ORIENTED_EDGE ( 'NONE', *, *, #18885, .F. ) ;
#34972=PRESENTATION_STYLE_ASSIGNMENT (( #15369 ) ) ;
#35018=ADVANCED_FACE ( 'NONE', ( #9073, #6228 ), #35676, .T. ) ;
#35035=DIRECTION ( 'NONE',  ( -1.734723475976807834E-16, 1.000000000000000000, 0.000000000000000000 ) ) ;
#35078=MECHANICAL_DESIGN_GEOMETRIC_PRESENTATION_REPRESENTATION('',(#42040),#12122);
#35212=AXIS2_PLACEMENT_3D ( 'NONE', #24046, #10943, #24488 ) ;
#35338=CIRCLE ( 'NONE', #16563, 19.19999999999999218 ) ;
#35342=VECTOR ( 'NONE', #6876, 1000.000000000000000 ) ;
#35344=ORIENTED_EDGE ( 'NONE', *, *, #37138, .F. ) ;
#35466=DIRECTION ( 'NONE',  ( 1.000000000000000000, 1.836909530733573776E-16, 0.000000000000000000 ) ) ;
#35481=VECTOR ( 'NONE', #37620, 1000.000000000000000 ) ;
#35573=DIRECTION ( 'NONE',  ( -1.847415842360817484E-16, 1.000000000000000000, 0.000000000000000000 ) ) ;
#35630=VERTEX_POINT ( 'NONE', #6592 ) ;
#35648=EDGE_LOOP ( 'NONE', ( #2484, #29444, #39313, #24845, #4226 ) ) ;
#35661=AXIS2_PLACEMENT_3D ( 'NONE', #31283, #21507, #21918 ) ;
#35676=PLANE ( 'NONE',  #5349 ) ;
#35717=SURFACE_SIDE_STYLE ('',( #42485 ) ) ;
#35767=TOROIDAL_SURFACE ( 'NONE', #37189, 15.08402000000000065, 0.08401999999999888724 ) ;
#35786=ORIENTED_EDGE ( 'NONE', *, *, #24802, .T. ) ;
#35846=ORIENTED_EDGE ( 'NONE', *, *, #36161, .T. ) ;
#35876=CIRCLE ( 'NONE', #24832, 19.19999999999999574 ) ;
#35934=( NAMED_UNIT ( * ) PLANE_ANGLE_UNIT ( ) SI_UNIT ( $, .RADIAN. ) );
#35950=CIRCLE ( 'NONE', #14378, 19.99999999999999645 ) ;
#36161=EDGE_CURVE ( 'NONE', #29681, #4294, #8960, .T. ) ;
#36259=DIRECTION ( 'NONE',  ( 0.000000000000000000, 0.000000000000000000, -1.000000000000000000 ) ) ;
#36266=FACE_BOUND ( 'NONE', #25076, .T. ) ;
#36365=FILL_AREA_STYLE_COLOUR ( '', #37367 ) ;
#36394=AXIS2_PLACEMENT_3D ( 'NONE', #14826, #37697, #24886 ) ;
#36437=CARTESIAN_POINT ( 'NONE',  ( 6.199999999999993960, 18.77999999999999758, 0.000000000000000000 ) ) ;
#36440=DIRECTION ( 'NONE',  ( -1.836909530733573776E-16, 1.000000000000000000, 0.000000000000000000 ) ) ;
#36488=PRODUCT_DEFINITION_FORMATION_WITH_SPECIFIED_SOURCE ( 'ANY', '', #9892, .NOT_KNOWN. ) ;
#36558=VERTEX_POINT ( 'NONE', #26967 ) ;
#36595=CARTESIAN_POINT ( 'NONE',  ( 5.991980000000000750, 1.836970198721029983E-15, -15.00000000000000355 ) ) ;
#36666=DIRECTION ( 'NONE',  ( 0.000000000000000000, 0.000000000000000000, 1.000000000000000000 ) ) ;
#36719=ORIENTED_EDGE ( 'NONE', *, *, #25333, .T. ) ;
#36730=DIRECTION ( 'NONE',  ( 0.000000000000000000, 0.000000000000000000, 1.000000000000000000 ) ) ;
#36734=FACE_OUTER_BOUND ( 'NONE', #3305, .T. ) ;
#36751=EDGE_CURVE ( 'NONE', #38331, #19229, #31985, .T. ) ;
#36768=EDGE_CURVE ( 'NONE', #17054, #40002, #8987, .T. ) ;
#36870=DIRECTION ( 'NONE',  ( -1.807003620809174385E-16, 1.000000000000000000, 0.000000000000000000 ) ) ;
#37013=VERTEX_POINT ( 'NONE', #26483 ) ;
#37138=EDGE_CURVE ( 'NONE', #36558, #9440, #13243, .T. ) ;
#37164=EDGE_LOOP ( 'NONE', ( #31516, #15546, #22947, #39951 ) ) ;
#37189=AXIS2_PLACEMENT_3D ( 'NONE', #9703, #6852, #29567 ) ;
#37263=CARTESIAN_POINT ( 'NONE',  ( 6.200000000000001066, -18.77999999999998337, 2.299886688798728323E-15 ) ) ;
#37282=CARTESIAN_POINT ( 'NONE',  ( -6.199999999999993960, -18.77999999999999048, 2.299886688798728717E-15 ) ) ;
#37367=COLOUR_RGB ( '', 0.40784314, 0.44705882, 0.49803922) ;
#37377=AXIS2_PLACEMENT_3D ( 'NONE', #58, #40635, #23899 ) ;
#37387=FACE_OUTER_BOUND ( 'NONE', #32631, .T. ) ;
#37396=EDGE_LOOP ( 'NONE', ( #27023, #144, #34290, #5058 ) ) ;
#37619=CARTESIAN_POINT ( 'NONE',  ( -31.74999999999999289, -19.19999999999999574, 2.351321854362917684E-15 ) ) ;
#37620=DIRECTION ( 'NONE',  ( 1.000000000000000000, 1.836909530733573776E-16, 0.000000000000000000 ) ) ;
#37697=DIRECTION ( 'NONE',  ( 1.000000000000000000, 1.836909530733573776E-16, 0.000000000000000000 ) ) ;
#37740=FACE_OUTER_BOUND ( 'NONE', #17867, .T. ) ;
#37842=ORIENTED_EDGE ( 'NONE', *, *, #30603, .T. ) ;
#37852=APPLICATION_CONTEXT ( 'automotive_design' ) ;
#38036=DIRECTION ( 'NONE',  ( -1.000000000000000000, 0.000000000000000000, 0.000000000000000000 ) ) ;
#38059=DIRECTION ( 'NONE',  ( 0.000000000000000000, 1.000000000000000000, 1.224646799147353207E-16 ) ) ;
#38066=CARTESIAN_POINT ( 'NONE',  ( -5.991980000000000750, 0.000000000000000000, 14.99999999999999822 ) ) ;
#38074=CIRCLE ( 'NONE', #13003, 19.59999999999999076 ) ;
#38110=AXIS2_PLACEMENT_3D ( 'NONE', #15797, #12097, #22789 ) ;
#38147=CIRCLE ( 'NONE', #22156, 0.08402000000000062196 ) ;
#38156=DIRECTION ( 'NONE',  ( 0.000000000000000000, 0.000000000000000000, -1.000000000000000000 ) ) ;
#38210=ADVANCED_FACE ( 'NONE', ( #10654 ), #31330, .T. ) ;
#38223=ORIENTED_EDGE ( 'NONE', *, *, #20621, .T. ) ;
#38241=DIRECTION ( 'NONE',  ( 1.000000000000000000, 1.836909530733573776E-16, 0.000000000000000000 ) ) ;
#38313=CIRCLE ( 'NONE', #27884, 0.08402000000000062196 ) ;
#38314=DIRECTION ( 'NONE',  ( 1.000000000000000000, 1.836909530733573776E-16, 0.000000000000000000 ) ) ;
#38316=CARTESIAN_POINT ( 'NONE',  ( 5.991980000000000750, 1.847259681127465666E-15, -15.08402000000000065 ) ) ;
#38321=VERTEX_POINT ( 'NONE', #8457 ) ;
#38331=VERTEX_POINT ( 'NONE', #31815 ) ;
#38346=AXIS2_PLACEMENT_3D ( 'NONE', #41854, #8049, #42054 ) ;
#38363=DIRECTION ( 'NONE',  ( -1.000000000000000000, 0.000000000000000000, 0.000000000000000000 ) ) ;
#38394=EDGE_CURVE ( 'NONE', #2759, #38331, #38313, .T. ) ;
#38460=DIRECTION ( 'NONE',  ( 0.000000000000000000, 0.000000000000000000, 1.000000000000000000 ) ) ;
#38501=CARTESIAN_POINT ( 'NONE',  ( -25.39999999999999147, 0.000000000000000000, 0.000000000000000000 ) ) ;
#38709=CARTESIAN_POINT ( 'NONE',  ( 7.000000000000002665, 19.59999999999999787, 0.000000000000000000 ) ) ;
#38717=FACE_OUTER_BOUND ( 'NONE', #15950, .T. ) ;
#38865=DIRECTION ( 'NONE',  ( 1.000000000000000000, 0.000000000000000000, 0.000000000000000000 ) ) ;
#38883=( NAMED_UNIT ( * ) SI_UNIT ( $, .STERADIAN. ) SOLID_ANGLE_UNIT ( ) );
#38941=DIRECTION ( 'NONE',  ( 1.000000000000000000, 1.836909530733573776E-16, 0.000000000000000000 ) ) ;
#38942=EDGE_CURVE ( 'NONE', #15674, #39595, #32762, .T. ) ;
#38963=DIRECTION ( 'NONE',  ( 1.000000000000000000, 1.836909530733573776E-16, 0.000000000000000000 ) ) ;
#39005=DIRECTION ( 'NONE',  ( 1.000000000000000000, 1.836909530733573776E-16, 0.000000000000000000 ) ) ;
#39027=UNCERTAINTY_MEASURE_WITH_UNIT (LENGTH_MEASURE( 1.000000000000000082E-05 ), #41067, 'distance_accuracy_value', 'NONE');
#39050=DIRECTION ( 'NONE',  ( -1.770125995894701695E-16, 1.000000000000000000, 0.000000000000000000 ) ) ;
#39144=DIRECTION ( 'NONE',  ( 0.000000000000000000, 1.000000000000000000, 1.224646799147353207E-16 ) ) ;
#39214=DIRECTION ( 'NONE',  ( 0.000000000000000000, 0.000000000000000000, 1.000000000000000000 ) ) ;
#39313=ORIENTED_EDGE ( 'NONE', *, *, #4911, .T. ) ;
#39320=VERTEX_POINT ( 'NONE', #17399 ) ;
#39336=TOROIDAL_SURFACE ( 'NONE', #17098, 19.59999999999999432, 0.4000000000000001887 ) ;
#39480=DIRECTION ( 'NONE',  ( 1.000000000000000000, 1.836909530733573776E-16, 0.000000000000000000 ) ) ;
#39536=DIRECTION ( 'NONE',  ( 0.000000000000000000, -1.000000000000000000, 0.000000000000000000 ) ) ;
#39543=ORIENTED_EDGE ( 'NONE', *, *, #20931, .T. ) ;
#39595=VERTEX_POINT ( 'NONE', #38066 ) ;
#39747=ORIENTED_EDGE ( 'NONE', *, *, #20661, .F. ) ;
#39768=EDGE_CURVE ( 'NONE', #38321, #2759, #12670, .T. ) ;
#39769=CARTESIAN_POINT ( 'NONE',  ( -6.004904395537136175, 2.351321854362917684E-15, -19.19999999999999574 ) ) ;
#39795=CARTESIAN_POINT ( 'NONE',  ( -31.75000000000000000, 18.77999999999999048, 0.000000000000000000 ) ) ;
#39798=DIRECTION ( 'NONE',  ( 1.000000000000000000, 1.836909530733573776E-16, 0.000000000000000000 ) ) ;
#39851=FACE_OUTER_BOUND ( 'NONE', #33661, .T. ) ;
#39934=DIRECTION ( 'NONE',  ( 0.000000000000000000, 0.000000000000000000, 1.000000000000000000 ) ) ;
#39951=ORIENTED_EDGE ( 'NONE', *, *, #9342, .F. ) ;
#40002=VERTEX_POINT ( 'NONE', #31052 ) ;
#40113=STYLED_ITEM ( 'NONE', ( #12838 ), #28662 ) ;
#40279=AXIS2_PLACEMENT_3D ( 'NONE', #22641, #5798, #16083 ) ;
#40343=DIRECTION ( 'NONE',  ( 0.000000000000000000, -1.000000000000000000, 0.000000000000000000 ) ) ;
#40348=FACE_OUTER_BOUND ( 'NONE', #5589, .T. ) ;
#40438=ADVANCED_FACE ( 'NONE', ( #19443 ), #34262, .T. ) ;
#40571=CYLINDRICAL_SURFACE ( 'NONE', #35212, 19.19999999999999574 ) ;
#40633=CARTESIAN_POINT ( 'NONE',  ( 6.004904395537136175, 0.000000000000000000, 0.000000000000000000 ) ) ;
#40635=DIRECTION ( 'NONE',  ( 1.000000000000000000, 0.000000000000000000, 0.000000000000000000 ) ) ;
#40719=DIRECTION ( 'NONE',  ( 0.000000000000000000, 0.000000000000000000, 1.000000000000000000 ) ) ;
#40722=DIRECTION ( 'NONE',  ( -1.000000000000000000, 0.000000000000000000, 0.000000000000000000 ) ) ;
#40735=CARTESIAN_POINT ( 'NONE',  ( 6.600000000000008527, 6.938893903907228378E-15, 0.000000000000000000 ) ) ;
#40778=CYLINDRICAL_SURFACE ( 'NONE', #31895, 15.00000000000000000 ) ;
#40781=DIRECTION ( 'NONE',  ( 1.000000000000000000, 1.836909530733573776E-16, 0.000000000000000000 ) ) ;
#40811=CIRCLE ( 'NONE', #2495, 19.11697999999999809 ) ;
#40864=AXIS2_PLACEMENT_3D ( 'NONE', #1386, #38036, #4664 ) ;
#40888=LINE ( 'NONE', #24369, #35481 ) ;
#40931=VERTEX_POINT ( 'NONE', #1030 ) ;
#40959=VERTEX_POINT ( 'NONE', #37263 ) ;
#41035=DIRECTION ( 'NONE',  ( -1.000000000000000000, 0.000000000000000000, 0.000000000000000000 ) ) ;
#41048=ORIENTED_EDGE ( 'NONE', *, *, #31173, .T. ) ;
#41051=DIRECTION ( 'NONE',  ( -1.000000000000000000, 0.000000000000000000, 0.000000000000000000 ) ) ;
#41061=FACE_OUTER_BOUND ( 'NONE', #32314, .T. ) ;
#41067=( LENGTH_UNIT ( ) NAMED_UNIT ( * ) SI_UNIT ( .MILLI., .METRE. ) );
#41075=VERTEX_POINT ( 'NONE', #39769 ) ;
#41231=EDGE_CURVE ( 'NONE', #28909, #30619, #23875, .T. ) ;
#41346=ADVANCED_FACE ( 'NONE', ( #5074 ), #21094, .T. ) ;
#41407=ADVANCED_FACE ( 'NONE', ( #41061 ), #14816, .T. ) ;
#41439=FACE_OUTER_BOUND ( 'NONE', #30390, .T. ) ;
#41579=DIRECTION ( 'NONE',  ( 1.000000000000000000, 1.836909530733573776E-16, 0.000000000000000000 ) ) ;
#41732=ORIENTED_EDGE ( 'NONE', *, *, #20578, .T. ) ;
#41761=CARTESIAN_POINT ( 'NONE',  ( -5.991980000000000750, 1.847259681127465666E-15, -15.08402000000000065 ) ) ;
#41812=DIRECTION ( 'NONE',  ( -1.847415842360817977E-16, 1.000000000000000000, 0.000000000000000000 ) ) ;
#41854=CARTESIAN_POINT ( 'NONE',  ( -5.991980000000000750, 0.000000000000000000, 0.000000000000000000 ) ) ;
#41871=ORIENTED_EDGE ( 'NONE', *, *, #11556, .F. ) ;
#41900=EDGE_CURVE ( 'NONE', #40959, #13405, #42948, .T. ) ;
#41926=CARTESIAN_POINT ( 'NONE',  ( -6.200000000000001066, 19.19999999999999929, 0.000000000000000000 ) ) ;
#41941=ORIENTED_EDGE ( 'NONE', *, *, #22784, .T. ) ;
#41951=CYLINDRICAL_SURFACE ( 'NONE', #38110, 18.77999999999999048 ) ;
#41986=CARTESIAN_POINT ( 'NONE',  ( -6.004904395537136175, 0.000000000000000000, 0.000000000000000000 ) ) ;
#42040=STYLED_ITEM ( 'NONE', ( #34972 ), #10920 ) ;
#42054=DIRECTION ( 'NONE',  ( 0.000000000000000000, 0.000000000000000000, 1.000000000000000000 ) ) ;
#42138=FILL_AREA_STYLE_COLOUR ( '', #28838 ) ;
#42148=CIRCLE ( 'NONE', #31028, 0.08401999999999715252 ) ;
#42193=CARTESIAN_POINT ( 'NONE',  ( 6.075999999999997847, 0.000000000000000000, 19.11697999999999809 ) ) ;
#42269=ORIENTED_EDGE ( 'NONE', *, *, #11556, .T. ) ;
#42485=SURFACE_STYLE_FILL_AREA ( #9328 ) ;
#42492=ORIENTED_EDGE ( 'NONE', *, *, #9475, .F. ) ;
#42562=CIRCLE ( 'NONE', #34927, 19.19999999999999574 ) ;
#42589=VERTEX_POINT ( 'NONE', #30696 ) ;
#42596=EDGE_LOOP ( 'NONE', ( #19336, #17565 ) ) ;
#42628=CARTESIAN_POINT ( 'NONE',  ( 5.991979999999993645, 2.341154836636396601E-15, -19.11697999999999809 ) ) ;
#42635=LINE ( 'NONE', #16068, #13564 ) ;
#42721=DIRECTION ( 'NONE',  ( 1.000000000000000000, 1.836909530733573776E-16, 0.000000000000000000 ) ) ;
#42784=ORIENTED_EDGE ( 'NONE', *, *, #38942, .T. ) ;
#42810=AXIS2_PLACEMENT_3D ( 'NONE', #40633, #10781, #36730 ) ;
#42859=AXIS2_PLACEMENT_3D ( 'NONE', #38316, #15014, #1879 ) ;
#42864=LINE ( 'NONE', #10583, #26148 ) ;
#42921=CARTESIAN_POINT ( 'NONE',  ( 6.999999999999985789, 19.60000000000008313, 0.000000000000000000 ) ) ;
#42948=LINE ( 'NONE', #18825, #18353 ) ;
#42970=ADVANCED_FACE ( 'NONE', ( #36734 ), #35767, .T. ) ;
#43019=FACE_OUTER_BOUND ( 'NONE', #24332, .T. ) ;
#43043=DIRECTION ( 'NONE',  ( -1.000000000000000000, 0.000000000000000000, 0.000000000000000000 ) ) ;
#43079=DIRECTION ( 'NONE',  ( 1.000000000000000000, 1.836909530733573776E-16, 0.000000000000000000 ) ) ;
#43105=CIRCLE ( 'NONE', #30616, 19.99999999999999645 ) ;
#43129=EDGE_LOOP ( 'NONE', ( #22814, #15761 ) ) ;
ENDSEC;
END-ISO-10303-21;
